ISO-10303-21;
HEADER;
FILE_DESCRIPTION (('STEP AP214'),
    '1' );
FILE_NAME ('Drain Plug.step',
    '2026-10-09T12:49:55',
    ( '' ),
    ( '' ),
    'SwSTEP 2.0',
    'SolidWorks 2026',
    '' );
FILE_SCHEMA (( 'AUTOMOTIVE_DESIGN' ));
ENDSEC;

DATA;
#1=CARTESIAN_POINT ( 'NONE',  ( -244.7604950974910878, 8.603785962528602838, 8.365103762022689793 ) ) ;
#45=CARTESIAN_POINT ( 'NONE',  ( -248.8440518482232733, 9.943161799075943108, -6.718187330775476696 ) ) ;
#52=DIRECTION ( 'NONE',  ( 0.000000000000000000, -1.000000000000000000, 0.000000000000000000 ) ) ;
#62=CARTESIAN_POINT ( 'NONE',  ( -246.4289107134841004, -9.384359667671809291, -7.479355995036127247 ) ) ;
#69=CARTESIAN_POINT ( 'NONE',  ( -239.9450917581429792, -2.156506209390995021, 11.80463811257499884 ) ) ;
#123=ORIENTED_EDGE ( 'NONE', *, *, #7186, .T. ) ;
#129=CARTESIAN_POINT ( 'NONE',  ( -248.5349130519067558, -9.924317173753149035, -6.749248572539269020 ) ) ;
#133=CARTESIAN_POINT ( 'NONE',  ( -244.3545189613893172, 8.356296381722604139, -8.612604416346371750 ) ) ;
#194=CARTESIAN_POINT ( 'NONE',  ( -244.9313462844523315, 8.700834631118880225, -8.264179333829037688 ) ) ;
#210=CARTESIAN_POINT ( 'NONE',  ( -249.3376476200290028, -9.985526825745921542, 6.655116011123642927 ) ) ;
#241=CARTESIAN_POINT ( 'NONE',  ( -233.0000000000000000, 1.000000000000000000, 11.95826074310140008 ) ) ;
#242=CARTESIAN_POINT ( 'NONE',  ( -243.4813404522815574, 7.728679802368522367, 9.179736092244874968 ) ) ;
#255=ORIENTED_EDGE ( 'NONE', *, *, #1182, .T. ) ;
#256=CARTESIAN_POINT ( 'NONE',  ( -233.0000000000000000, 0.000000000000000000, 0.000000000000000000 ) ) ;
#257=CARTESIAN_POINT ( 'NONE',  ( -241.6004288480548610, 5.767183905335713234, -10.52387470031727368 ) ) ;
#258=CARTESIAN_POINT ( 'NONE',  ( -238.7266973618091299, 0.3758472202226714187, 11.99420542475303009 ) ) ;
#263=CARTESIAN_POINT ( 'NONE',  ( -229.6996873213522008, 2.466058644897756835, -11.74980236389214028 ) ) ;
#271=CARTESIAN_POINT ( 'NONE',  ( -233.0000000000000000, -1.000000000000000000, -11.95826074310140008 ) ) ;
#277=CARTESIAN_POINT ( 'NONE',  ( -247.9991062040697045, -9.816924796812509513, 6.901310522868776332 ) ) ;
#286=CARTESIAN_POINT ( 'NONE',  ( -249.7118339206215012, -9.997999799959989886, 6.636264009214830395 ) ) ;
#317=CARTESIAN_POINT ( 'NONE',  ( -243.1855895756006589, 7.483404894430283782, 9.380758043284854963 ) ) ;
#329=CARTESIAN_POINT ( 'NONE',  ( -239.9450917581424960, 2.156506209390990136, -11.80463811257499884 ) ) ;
#330=CARTESIAN_POINT ( 'NONE',  ( -239.9450917581424960, 2.156506209390990136, 11.80463811257499884 ) ) ;
#384=LINE ( 'NONE', #12452, #9582 ) ;
#388=CARTESIAN_POINT ( 'NONE',  ( -244.8267157023690004, 8.641841620762505727, -8.325778331754211337 ) ) ;
#414=CARTESIAN_POINT ( 'NONE',  ( 0.000000000000000000, -13.19999999999999929, 0.000000000000000000 ) ) ;
#444=SURFACE_STYLE_USAGE ( .BOTH. , #9562 ) ;
#459=CARTESIAN_POINT ( 'NONE',  ( -247.5810890924702790, -9.727605306517407513, -7.026623146109774787 ) ) ;
#488=CARTESIAN_POINT ( 'NONE',  ( -239.9450917581424960, 2.156506209390990136, 11.80463811257499884 ) ) ;
#503=AXIS2_PLACEMENT_3D ( 'NONE', #10733, #3595, #9864 ) ;
#523=CARTESIAN_POINT ( 'NONE',  ( -239.4244912090118191, 1.754035804298239798, 11.87111434752389272 ) ) ;
#525=CARTESIAN_POINT ( 'NONE',  ( -247.9423986614758348, -9.805815554863000827, 6.917079555584196626 ) ) ;
#527=CARTESIAN_POINT ( 'NONE',  ( -229.9856741818797445, 11.72241588658361167, -2.593326906271713916 ) ) ;
#542=CARTESIAN_POINT ( 'NONE',  ( -241.2764277293246664, 5.294572826602574445, 10.76882343127053865 ) ) ;
#547=CARTESIAN_POINT ( 'NONE',  ( -241.1581829739467366, -5.108108803544517684, -10.85886904366963712 ) ) ;
#585=AXIS2_PLACEMENT_3D ( 'NONE', #11911, #2760, #6847 ) ;
#609=CARTESIAN_POINT ( 'NONE',  ( -241.2764277293045438, -5.294572826571302571, -10.76882343128240471 ) ) ;
#644=VERTEX_POINT ( 'NONE', #944 ) ;
#652=CARTESIAN_POINT ( 'NONE',  ( -240.6982673023520647, -4.277714796963365984, 11.21297710688243399 ) ) ;
#653=DIRECTION ( 'NONE',  ( 1.000000000000000000, 0.000000000000000000, 0.000000000000000000 ) ) ;
#669=CARTESIAN_POINT ( 'NONE',  ( -240.7195678459729038, 4.326096554678287021, 11.19626641897951913 ) ) ;
#693=B_SPLINE_CURVE_WITH_KNOTS ( 'NONE', 3,
 ( #6931, #991, #9191, #10178, #8995, #7922, #45, #1993, #11102, #3922, #7996, #12056, #7131, #2907, #12262, #6065, #6992, #4985, #4052, #10118, #9120, #4121, #11056, #11186, #1927, #930, #12192, #5998, #2053, #6123, #1055, #8201, #3111, #7188, #11254, #2117, #9924, #1323, #4184, #11323, #194, #1388, #5320, #12517, #388, #6267, #4251, #1195, #5451, #133, #2186, #6328, #11592, #3439, #12325, #11455, #10519, #4440, #4382, #12457, #10452, #3177, #2312, #3310, #6194, #3370, #7519, #7388, #7453, #6395, #8264, #7258, #10248, #10316, #12583, #9457, #10378, #257, #8331, #1124, #8524, #8463, #5389, #5251, #9322, #12389, #11528, #5181, #3243, #9260, #7325, #11394, #2254, #1256, #2383, #9513, #329 ),
 .UNSPECIFIED., .F., .F.,
 ( 4, 1, 1, 2, 2, 2, 1, 1, 1, 2, 2, 2, 2, 1, 1, 1, 2, 2, 2, 1, 1, 1, 2, 2, 2, 1, 1, 1, 1, 2, 2, 2, 1, 1, 1, 2, 2, 1, 1, 1, 1, 2, 2, 2, 2, 1, 1, 1, 2, 2, 2, 2, 1, 1, 1, 2, 2, 2, 1, 1, 1, 2, 2, 4 ),
 ( 0.000000000000000000, 0.03124999999996640881, 0.04687499999994677174, 0.05468749999993696015, 0.06249999999992715549, 0.09374999999987633503, 0.1093749999998509387, 0.1171874999998381989, 0.1210937499998318428, 0.1230468749998313432, 0.1249999999998308575, 0.1874999999996515565, 0.2187499999995618505, 0.2343749999995169975, 0.2421874999994945710, 0.2460937499994810540, 0.2480468749994765854, 0.2499999999994720890, 0.2812499999993741118, 0.2968749999993226529, 0.3046874999992970623, 0.3085937499992819633, 0.3105468749992766342, 0.3124999999992712496, 0.3437499999991869837, 0.3593749999991447397, 0.3671874999991236455, 0.3710937499991131538, 0.3730468749991098232, 0.3740234374991061039, 0.3749999999991024402, 0.4062499999991214250, 0.4218749999991309729, 0.4296874999991357469, 0.4335937499991380784, 0.4355468749991411870, 0.4374999999991442956, 0.4687499999992265631, 0.4843749999992656985, 0.4921874999992851829, 0.4960937499992930100, 0.4980468749992968958, 0.4999999999993007815, 0.5624999999994121369, 0.5937499999994678701, 0.6093749999994938493, 0.6171874999995067279, 0.6210937499995131672, 0.6230468749995142774, 0.6249999999995153876, 0.6874999999995312638, 0.7187499999995392574, 0.7343749999995432542, 0.7421874999995468070, 0.7460937499995484723, 0.7480468749995492495, 0.7499999999995500266, 0.8124999999996305178, 0.8437499999996695976, 0.8593749999996903588, 0.8671874999997019051, 0.8710937499997087885, 0.8749999999997156719, 1.000000000000000000 ),
 .UNSPECIFIED. ) ;
#713=STYLED_ITEM ( 'NONE', ( #5636 ), #10422 ) ;
#723=CARTESIAN_POINT ( 'NONE',  ( -244.1910629296142474, -8.248580890786996633, 8.715491051944391998 ) ) ;
#728=CARTESIAN_POINT ( 'NONE',  ( -229.7633312047737491, 5.934404468281496037, 10.43166704019080093 ) ) ;
#740=CARTESIAN_POINT ( 'NONE',  ( -241.5877467168933492, 5.754636832785866574, 10.53299718340092817 ) ) ;
#748=CARTESIAN_POINT ( 'NONE',  ( -229.9997816294760753, -11.99584946919181405, 0.3676194914965865146 ) ) ;
#784=CARTESIAN_POINT ( 'NONE',  ( -245.5461639313266744, -9.015782184408621447, 7.919169856991794099 ) ) ;
#805=AXIS2_PLACEMENT_3D ( 'NONE', #6711, #10765, #10635 ) ;
#806=CARTESIAN_POINT ( 'NONE',  ( -229.9857581487122218, -11.72407015423622489, -2.585718574142970017 ) ) ;
#820=CARTESIAN_POINT ( 'NONE',  ( -239.4731782950807712, -1.801843764861105646, 11.86393663232041540 ) ) ;
#832=CARTESIAN_POINT ( 'NONE',  ( -239.0397834240491477, -1.254461513564051556, -11.93425063537890374 ) ) ;
#850=CARTESIAN_POINT ( 'NONE',  ( -241.6809225226833462, -5.875971056079142052, 10.46353150752503502 ) ) ;
#851=CARTESIAN_POINT ( 'NONE',  ( -238.8090076341308361, 0.7315829127600046444, -11.97771329458992717 ) ) ;
#865=CARTESIAN_POINT ( 'NONE',  ( -246.4289107141176771, 9.384359667912798741, 7.479355994788029705 ) ) ;
#878=FACE_OUTER_BOUND ( 'NONE', #3268, .T. ) ;
#884=AXIS2_PLACEMENT_3D ( 'NONE', #12840, #5778, #12647 ) ;
#885=CARTESIAN_POINT ( 'NONE',  ( -239.4731783641827860, 1.801843830935816015, -11.86393662238275226 ) ) ;
#888=CARTESIAN_POINT ( 'NONE',  ( -239.0548353902184431, -1.279873199611678114, 11.93155240848446219 ) ) ;
#907=AXIS2_PLACEMENT_3D ( 'NONE', #1181, #52, #3230 ) ;
#916=CARTESIAN_POINT ( 'NONE',  ( -241.3090253319653016, -5.344653766038736542, 10.74405649903519055 ) ) ;
#918=CARTESIAN_POINT ( 'NONE',  ( -239.1644449882676042, 1.447449306433101768, -11.91236063194371830 ) ) ;
#930=CARTESIAN_POINT ( 'NONE',  ( -246.3126759744927483, 9.340233780095946514, -7.533927936320575114 ) ) ;
#933=CARTESIAN_POINT ( 'NONE',  ( 0.000000000000000000, 2.156506209390990136, 0.000000000000000000 ) ) ;
#934=CARTESIAN_POINT ( 'NONE',  ( -243.0176490155954809, 7.336472069124719830, 9.496559185463413044 ) ) ;
#944=CARTESIAN_POINT ( 'NONE',  ( -229.6889200636375108, 1.000000000000000000, 11.95826074310140008 ) ) ;
#981=CARTESIAN_POINT ( 'NONE',  ( -238.8461604313190492, 0.8432863473122946818, -11.97040126065660282 ) ) ;
#985=CARTESIAN_POINT ( 'NONE',  ( -247.9076433805199144, -9.798874666935999400, -6.926911304953004667 ) ) ;
#991=CARTESIAN_POINT ( 'NONE',  ( -249.5626403296618605, 9.995018771278006753, -6.640755139182748401 ) ) ;
#994=CARTESIAN_POINT ( 'NONE',  ( -243.3783983494642769, 7.645447681623645408, 9.249237797097162428 ) ) ;
#1024=CARTESIAN_POINT ( 'NONE',  ( -239.4312206625581609, -1.760784905609661166, -11.87011525670738266 ) ) ;
#1050=CARTESIAN_POINT ( 'NONE',  ( -249.1334134305279804, -9.986442412942713176, -6.653676027923776104 ) ) ;
#1055=CARTESIAN_POINT ( 'NONE',  ( -245.7661201680033116, 9.116795905909876652, -7.802929255001362030 ) ) ;
#1059=CARTESIAN_POINT ( 'NONE',  ( -246.9756885468848964, 9.564884955133036826, 7.246373649300591246 ) ) ;
#1081=PRODUCT_DEFINITION_FORMATION_WITH_SPECIFIED_SOURCE ( 'ANY', '', #6399, .NOT_KNOWN. ) ;
#1120=CARTESIAN_POINT ( 'NONE',  ( -243.3783983492338052, -7.645447681435416420, -9.249237797260425609 ) ) ;
#1124=CARTESIAN_POINT ( 'NONE',  ( -241.4289589285359909, 5.524154699870469365, -10.65313710557074600 ) ) ;
#1130=CARTESIAN_POINT ( 'NONE',  ( -229.7038372623077294, 2.825322550619665307, -11.66863389586242405 ) ) ;
#1143=CYLINDRICAL_SURFACE ( 'NONE', #4730, 12.00000000000000000 ) ;
#1181=CARTESIAN_POINT ( 'NONE',  ( 0.000000000000000000, 3.061616997868383141E-16, 0.000000000000000000 ) ) ;
#1182=EDGE_CURVE ( 'NONE', #4229, #4886, #693, .T. ) ;
#1186=DIRECTION ( 'NONE',  ( 1.000000000000000000, 0.000000000000000000, 0.000000000000000000 ) ) ;
#1195=CARTESIAN_POINT ( 'NONE',  ( -244.6143483605412712, 8.518413540729250499, -8.452629823371180962 ) ) ;
#1210=DIRECTION ( 'NONE',  ( 0.000000000000000000, -1.000000000000000000, 0.000000000000000000 ) ) ;
#1218=VERTEX_POINT ( 'NONE', #9698 ) ;
#1248=CARTESIAN_POINT ( 'NONE',  ( -246.2769436246209125, -9.326692435563586514, -7.550684327968305354 ) ) ;
#1256=CARTESIAN_POINT ( 'NONE',  ( -240.5058532487275329, 3.857938722303589696, -11.36295048183480283 ) ) ;
#1257=CARTESIAN_POINT ( 'NONE',  ( -238.8437317866286378, 0.8419213848770401576, 11.97081056113904651 ) ) ;
#1263=CARTESIAN_POINT ( 'NONE',  ( -229.7434709365983565, 5.107855674974426385, -10.86021397319516169 ) ) ;
#1266=VECTOR ( 'NONE', #8246, 1000.000000000000000 ) ;
#1275=CARTESIAN_POINT ( 'NONE',  ( -246.6520855341642289, -9.461709548621238142, 7.381047753367473874 ) ) ;
#1277=ADVANCED_FACE ( 'NONE', ( #8845 ), #9181, .F. ) ;
#1284=VECTOR ( 'NONE', #12599, 1000.000000000000000 ) ;
#1309=CARTESIAN_POINT ( 'NONE',  ( -247.0236966368111950, 9.579141830482246434, 7.227478268527401717 ) ) ;
#1323=CARTESIAN_POINT ( 'NONE',  ( -245.3145835528066812, 8.904103459659600261, -8.045132556734525764 ) ) ;
#1324=CARTESIAN_POINT ( 'NONE',  ( -238.6985546676629326, 0.1065515246389758391, 11.99999998203097107 ) ) ;
#1330=CARTESIAN_POINT ( 'NONE',  ( -229.8368610672713146, 8.310328450785883447, -8.664835459456435629 ) ) ;
#1350=CARTESIAN_POINT ( 'NONE',  ( -229.9335310080516592, -10.65269000883797190, 5.546765194287003986 ) ) ;
#1388=CARTESIAN_POINT ( 'NONE',  ( -244.8752249706953990, 8.669362157675379876, -8.297136228722845175 ) ) ;
#1397=CARTESIAN_POINT ( 'NONE',  ( -229.8757030161491741, 9.332370542760813237, -7.580342957207111709 ) ) ;
#1453=CARTESIAN_POINT ( 'NONE',  ( -229.8756056487268324, 9.317215184761726832, 7.564809101436958727 ) ) ;
#1489=AXIS2_PLACEMENT_3D ( 'NONE', #4138, #8410, #12472 ) ;
#1509=EDGE_LOOP ( 'NONE', ( #8706, #2553 ) ) ;
#1513=AXIS2_PLACEMENT_3D ( 'NONE', #11806, #4647, #6800 ) ;
#1518=FACE_OUTER_BOUND ( 'NONE', #11567, .T. ) ;
#1523=CARTESIAN_POINT ( 'NONE',  ( -229.9999846513224782, 11.99971501660928297, 0.7499535807134399823 ) ) ;
#1541=CARTESIAN_POINT ( 'NONE',  ( -240.2963067560461923, -3.341048620459575513, -11.52705098702835684 ) ) ;
#1559=ADVANCED_FACE ( 'NONE', ( #3226 ), #10628, .F. ) ;
#1562=ORIENTED_EDGE ( 'NONE', *, *, #5129, .F. ) ;
#1568=CARTESIAN_POINT ( 'NONE',  ( 0.000000000000000000, -13.19999999999999929, 0.000000000000000000 ) ) ;
#1574=SURFACE_STYLE_FILL_AREA ( #12504 ) ;
#1586=EDGE_CURVE ( 'NONE', #7801, #9902, #12304, .T. ) ;
#1604=CARTESIAN_POINT ( 'NONE',  ( -241.2922373263966733, 5.318940986329955933, 10.75680814016106268 ) ) ;
#1609=CARTESIAN_POINT ( 'NONE',  ( -241.2613930294912166, -5.271300103266470138, -10.78025408310512923 ) ) ;
#1644=CARTESIAN_POINT ( 'NONE',  ( -245.5963909204522224, -9.039317601314641237, 7.892311131002199609 ) ) ;
#1649=CARTESIAN_POINT ( 'NONE',  ( -229.7197234876223888, 3.908141881471038026, 11.35191153251636820 ) ) ;
#1657=( GEOMETRIC_REPRESENTATION_CONTEXT ( 3 ) GLOBAL_UNCERTAINTY_ASSIGNED_CONTEXT ( ( #4882 ) ) GLOBAL_UNIT_ASSIGNED_CONTEXT ( ( #2562, #6643, #5635 ) ) REPRESENTATION_CONTEXT ( 'NONE', 'WORKASPACE' ) );
#1671=CARTESIAN_POINT ( 'NONE',  ( -229.7894208366921021, -6.875096941970043396, -9.842338683517198206 ) ) ;
#1716=CARTESIAN_POINT ( 'NONE',  ( -245.1341653186248379, -8.810613775770821832, 8.147076446021827678 ) ) ;
#1717=CARTESIAN_POINT ( 'NONE',  ( -238.6985546661037176, 0.1084670113012983633, -12.00000001867801913 ) ) ;
#1759=CARTESIAN_POINT ( 'NONE',  ( -238.6985546649171397, -0.2132982402979453351, 12.00000003664865922 ) ) ;
#1776=ORIENTED_EDGE ( 'NONE', *, *, #4487, .F. ) ;
#1780=CLOSED_SHELL ( 'NONE', ( #12899, #2477, #4181, #9023, #10038, #1277, #3197, #1559, #10098, #7265, #4414, #11203, #10056 ) ) ;
#1782=DIRECTION ( 'NONE',  ( 1.000000000000000000, 0.000000000000000000, 0.000000000000000000 ) ) ;
#1783=CARTESIAN_POINT ( 'NONE',  ( -249.7379166007395384, -10.64944549071737612, -5.654815128212893782 ) ) ;
#1788=CARTESIAN_POINT ( 'NONE',  ( -244.0248830888179725, -8.135989420001664030, 8.821260460492251099 ) ) ;
#1811=B_SPLINE_CURVE_WITH_KNOTS ( 'NONE', 3,
 ( #2323, #6401, #8402, #263, #1130, #7330, #6468, #10459, #5457, #12462, #1263, #4321, #2258, #8530, #3315, #7393, #4447, #1330, #10525, #1397, #12590, #9518, #8269, #11261, #5188, #3185, #527, #7784, #11662, #4778, #7587, #7715, #1523, #8596, #12849, #2516, #10721, #5587, #9647, #4576, #10585, #8720, #8656, #5522, #1453, #6663, #2454, #7527, #6731, #3716, #8854, #11854, #12713, #3578, #9775, #728, #10781, #11795, #7649, #6530, #1649, #10847, #5788, #3447, #4708 ),
 .UNSPECIFIED., .F., .F.,
 ( 4, 2, 2, 2, 2, 2, 2, 2, 2, 2, 2, 2, 2, 2, 1, 2, 2, 2, 2, 2, 2, 2, 1, 2, 2, 1, 2, 2, 2, 2, 2, 2, 2, 4 ),
 ( 0.000000000000000000, 0.03125000000000011102, 0.06250000000000022204, 0.09375000000000036082, 0.1093750000000003886, 0.1250000000000004163, 0.1562500000000004718, 0.1875000000000005274, 0.2187500000000005829, 0.2500000000000006661, 0.3125000000000008882, 0.3750000000000011102, 0.4062500000000012212, 0.4375000000000013323, 0.4687500000000013878, 0.4843750000000014433, 0.5000000000000014433, 0.5625000000000016653, 0.5937500000000017764, 0.6250000000000018874, 0.6562500000000019984, 0.6875000000000021094, 0.7187500000000022204, 0.7343750000000021094, 0.7500000000000021094, 0.7812500000000018874, 0.7968750000000016653, 0.8125000000000015543, 0.8437500000000012212, 0.8593750000000009992, 0.8750000000000008882, 0.9062500000000006661, 0.9375000000000004441, 1.000000000000000000 ),
 .UNSPECIFIED. ) ;
#1813=CARTESIAN_POINT ( 'NONE',  ( -229.8369385731911905, -8.312474322141341077, -8.662778311384863983 ) ) ;
#1825=CARTESIAN_POINT ( 'NONE',  ( -239.4909294218351761, -1.818763037284782724, 11.86135881504065992 ) ) ;
#1838=CARTESIAN_POINT ( 'NONE',  ( -233.0000000000000000, 0.000000000000000000, 0.000000000000000000 ) ) ;
#1852=CARTESIAN_POINT ( 'NONE',  ( -241.3214569865913006, -5.363580936720061310, 10.73461844913211216 ) ) ;
#1867=CARTESIAN_POINT ( 'NONE',  ( -249.7915528516602990, 11.82778639354381767, 2.343958593093920850 ) ) ;
#1872=VERTEX_POINT ( 'NONE', #286 ) ;
#1879=DIRECTION ( 'NONE',  ( 0.000000000000000000, -1.000000000000000000, 0.000000000000000000 ) ) ;
#1914=CARTESIAN_POINT ( 'NONE',  ( -244.8216528716611435, -8.638952368812793381, 8.328775922993848724 ) ) ;
#1927=CARTESIAN_POINT ( 'NONE',  ( -246.3306884220363315, 9.347001913570167630, -7.525531261512992565 ) ) ;
#1931=CARTESIAN_POINT ( 'NONE',  ( -247.5810890934098722, 9.727605306738871249, 7.026623145748954080 ) ) ;
#1936=CARTESIAN_POINT ( 'NONE',  ( -229.9928432556552025, -11.86223413274156613, -1.851200411155011771 ) ) ;
#1952=CARTESIAN_POINT ( 'NONE',  ( -239.1349169607758540, -1.405155705096720498, 11.91743587386434733 ) ) ;
#1980=CARTESIAN_POINT ( 'NONE',  ( -239.4323407760790019, 1.761903430914204760, -11.86994927865681149 ) ) ;
#1985=CARTESIAN_POINT ( 'NONE',  ( -246.0976122657799010, -9.256780777540988936, -7.636466318229263806 ) ) ;
#1993=CARTESIAN_POINT ( 'NONE',  ( -248.6652334659176802, 9.923450224964128097, -6.747319396128238722 ) ) ;
#1997=CARTESIAN_POINT ( 'NONE',  ( -248.5349130529941704, 9.924317173972164952, 6.749248572508020239 ) ) ;
#2036=EDGE_CURVE ( 'NONE', #6295, #7466, #3961, .T. ) ;
#2053=CARTESIAN_POINT ( 'NONE',  ( -246.0505219334675076, 9.238338704539428292, -7.658960896126895790 ) ) ;
#2056=CARTESIAN_POINT ( 'NONE',  ( -247.8923716106052950, 9.795774998289056512, 6.931293060548126661 ) ) ;
#2081=EDGE_CURVE ( 'NONE', #1218, #11098, #384, .T. ) ;
#2086=CARTESIAN_POINT ( 'NONE',  ( -239.6349225386288708, -1.943794465495108703, -11.84155609468290571 ) ) ;
#2088=ORIENTED_EDGE ( 'NONE', *, *, #5129, .T. ) ;
#2106=ORIENTED_EDGE ( 'NONE', *, *, #4196, .F. ) ;
#2112=CARTESIAN_POINT ( 'NONE',  ( -243.0176490148521395, -7.336472068459895191, -9.496559186012056841 ) ) ;
#2117=CARTESIAN_POINT ( 'NONE',  ( -245.5461639313797377, 9.015782184433717816, -7.919169856962964715 ) ) ;
#2156=CARTESIAN_POINT ( 'NONE',  ( -239.4338636940265133, -1.763423114931361946, -11.86972337156385393 ) ) ;
#2186=CARTESIAN_POINT ( 'NONE',  ( -244.2463344858503831, 8.285434993257245750, -8.680536399821541238 ) ) ;
#2208=CARTESIAN_POINT ( 'NONE',  ( -248.1924789821139825, -9.852676062999542239, 6.850256174357434169 ) ) ;
#2234=VECTOR ( 'NONE', #7871, 1000.000000000000000 ) ;
#2236=CARTESIAN_POINT ( 'NONE',  ( 0.000000000000000000, 0.000000000000000000, 0.000000000000000000 ) ) ;
#2249=CARTESIAN_POINT ( 'NONE',  ( -244.7604950959731696, -8.603785961650375569, -8.365103762956266564 ) ) ;
#2254=CARTESIAN_POINT ( 'NONE',  ( -240.5118714936659501, 3.871746541805194841, -11.35824976271609188 ) ) ;
#2258=CARTESIAN_POINT ( 'NONE',  ( -229.7631465151204679, 5.933468005304723292, -10.43713253351459080 ) ) ;
#2267=CARTESIAN_POINT ( 'NONE',  ( -247.0023889732649991, -9.573823398995038758, 7.235426325582930751 ) ) ;
#2298=CARTESIAN_POINT ( 'NONE',  ( -246.8626574257879156, 9.530421749008032961, 7.291787928144687569 ) ) ;
#2308=ORIENTED_EDGE ( 'NONE', *, *, #5737, .F. ) ;
#2312=CARTESIAN_POINT ( 'NONE',  ( -243.4994605516075978, 7.743136871922250641, -9.167522614886454591 ) ) ;
#2323=CARTESIAN_POINT ( 'NONE',  ( -229.6889200636375108, 1.000000000000000000, -11.95826074310140008 ) ) ;
#2383=CARTESIAN_POINT ( 'NONE',  ( -240.2579444297316797, 3.284593558773872157, -11.55663755354172295 ) ) ;
#2384=CARTESIAN_POINT ( 'NONE',  ( -239.4103023865795592, 1.739665387982153755, 11.87322930970978518 ) ) ;
#2440=EDGE_LOOP ( 'NONE', ( #9151, #9297, #2088, #9387 ) ) ;
#2447=CARTESIAN_POINT ( 'NONE',  ( -238.6985546758615442, -1.431921744593627863E-13, 12.00000000011287504 ) ) ;
#2454=CARTESIAN_POINT ( 'NONE',  ( -229.8611669809016007, 8.953871400566880467, 7.991408290370279666 ) ) ;
#2458=ORIENTED_EDGE ( 'NONE', *, *, #4437, .F. ) ;
#2467=EDGE_CURVE ( 'NONE', #4948, #11098, #3421, .T. ) ;
#2471=CARTESIAN_POINT ( 'NONE',  ( -242.0646888574074467, -6.354939414423857791, -10.17926273101336143 ) ) ;
#2477=ADVANCED_FACE ( 'NONE', ( #7641 ), #11719, .T. ) ;
#2498=CARTESIAN_POINT ( 'NONE',  ( -249.7800409167776934, 11.57739048715638397, -3.170426907196378430 ) ) ;
#2508=CARTESIAN_POINT ( 'NONE',  ( -239.0092219884379858, 1.200944422457546068, 11.93976291956724900 ) ) ;
#2511=CARTESIAN_POINT ( 'NONE',  ( -246.3126759746303946, -9.340233780147908504, 7.533927936259328995 ) ) ;
#2516=CARTESIAN_POINT ( 'NONE',  ( -229.9813512810838461, 11.63766203094939300, 2.950567834083252627 ) ) ;
#2536=CARTESIAN_POINT ( 'NONE',  ( -240.9204428195482137, -4.702057767565119839, -11.04114865042053317 ) ) ;
#2553=ORIENTED_EDGE ( 'NONE', *, *, #6938, .T. ) ;
#2562=( LENGTH_UNIT ( ) NAMED_UNIT ( * ) SI_UNIT ( .MILLI., .METRE. ) );
#2596=CARTESIAN_POINT ( 'NONE',  ( -240.4621951198754175, -3.755930367947129422, -11.39707303937288785 ) ) ;
#2597=DIRECTION ( 'NONE',  ( 0.000000000000000000, -1.000000000000000000, 0.000000000000000000 ) ) ;
#2614=ORIENTED_EDGE ( 'NONE', *, *, #2081, .F. ) ;
#2632=ORIENTED_EDGE ( 'NONE', *, *, #11572, .T. ) ;
#2637=CARTESIAN_POINT ( 'NONE',  ( -244.1671264040621168, -8.232476464565948504, 8.730683391379466585 ) ) ;
#2653=CARTESIAN_POINT ( 'NONE',  ( -242.1349625647511346, 6.437046976376021412, 10.12773524473490916 ) ) ;
#2661=CARTESIAN_POINT ( 'NONE',  ( -229.7228301394881953, -4.075732016279721037, -11.28829787118005257 ) ) ;
#2697=CARTESIAN_POINT ( 'NONE',  ( -244.1419029264688447, -8.215433989563221573, 8.746719778172643345 ) ) ;
#2711=CARTESIAN_POINT ( 'NONE',  ( -241.2613930295258911, 5.271300103320590402, 10.78025408308435118 ) ) ;
#2719=CARTESIAN_POINT ( 'NONE',  ( -242.2842939340737303, -6.604577240716344555, -10.01896504309209490 ) ) ;
#2720=CARTESIAN_POINT ( 'NONE',  ( -229.7140399059962590, -3.545728899456203287, -11.46574107171501211 ) ) ;
#2736=CARTESIAN_POINT ( 'NONE',  ( -238.7263736996250145, -0.4312313169119866840, 11.99417204546059246 ) ) ;
#2760=DIRECTION ( 'NONE',  ( 0.000000000000000000, -1.000000000000000000, 0.000000000000000000 ) ) ;
#2763=CARTESIAN_POINT ( 'NONE',  ( -244.4430806032956127, -8.412306923258608293, 8.557769328622804039 ) ) ;
#2767=PRODUCT_DEFINITION ( 'UNKNOWN', '', #1081, #5963 ) ;
#2789=CARTESIAN_POINT ( 'NONE',  ( -229.9653387109620724, -11.31703423231781080, 4.007864545467224815 ) ) ;
#2797=PLANE ( 'NONE',  #8591 ) ;
#2832=CARTESIAN_POINT ( 'NONE',  ( -240.7937243743992326, -4.465328607175659492, 11.13898957083963381 ) ) ;
#2833=CARTESIAN_POINT ( 'NONE',  ( -239.2621195177060827, 1.577673499042776539, -11.89604841323225948 ) ) ;
#2856=CARTESIAN_POINT ( 'NONE',  ( -229.9875200610103434, -11.75842346339721800, 2.402998940429985630 ) ) ;
#2876=LINE ( 'NONE', #5832, #5518 ) ;
#2883=CARTESIAN_POINT ( 'NONE',  ( -238.6985546673921021, -0.1083677397390090530, -11.99999998179152172 ) ) ;
#2897=CARTESIAN_POINT ( 'NONE',  ( -245.5719560650741187, -9.027896078068753383, 7.905358857528972827 ) ) ;
#2898=CARTESIAN_POINT ( 'NONE',  ( -238.7338796418129050, 0.4303581359859351418, -11.99273839260487406 ) ) ;
#2907=CARTESIAN_POINT ( 'NONE',  ( -247.9713910025420489, 9.811523844255248150, -6.908981293660537482 ) ) ;
#2911=CARTESIAN_POINT ( 'NONE',  ( -242.4509935387671078, 6.787150506580164055, 9.898021028034207802 ) ) ;
#2927=DIRECTION ( 'NONE',  ( -1.000000000000000000, 0.000000000000000000, 0.000000000000000000 ) ) ;
#2936=CARTESIAN_POINT ( 'NONE',  ( -238.9765878214913073, -1.145734732244408693, 11.94560817762122618 ) ) ;
#2953=ORIENTED_EDGE ( 'NONE', *, *, #10291, .T. ) ;
#2969=ORIENTED_EDGE ( 'NONE', *, *, #7066, .T. ) ;
#2974=CARTESIAN_POINT ( 'NONE',  ( -243.4562500151471056, -7.708554438499255035, -9.196640587784429499 ) ) ;
#2983=CARTESIAN_POINT ( 'NONE',  ( -247.3711767300066811, 9.676486748390463077, 7.096931842783562594 ) ) ;
#3006=CARTESIAN_POINT ( 'NONE',  ( -238.8209209931138446, -0.7687232751576088541, 11.97535954172162853 ) ) ;
#3050=CARTESIAN_POINT ( 'NONE',  ( -243.4720072945636389, 7.721209754011274740, 9.186020676430386445 ) ) ;
#3083=CARTESIAN_POINT ( 'NONE',  ( -239.9450917581429792, -2.156506209390995021, -11.80463811257499884 ) ) ;
#3092=AXIS2_PLACEMENT_3D ( 'NONE', #9737, #12812, #7751 ) ;
#3093=B_SPLINE_CURVE_WITH_KNOTS ( 'NONE', 3,
 ( #5826, #10956, #9886, #4810, #7811, #3816, #10018, #5892, #11955, #6025, #9086, #1825, #820, #7956, #11085, #3642, #12025, #4884, #8956, #4007, #13018, #8090, #5960, #1952, #6955, #11014, #888, #4947, #8548, #3949, #2936, #5757, #7021, #12152, #3006, #8823, #10814, #9815, #11884, #2736, #1759, #12479 ),
 .UNSPECIFIED., .F., .F.,
 ( 4, 2, 2, 2, 2, 2, 2, 1, 1, 1, 2, 2, 2, 2, 1, 1, 2, 2, 2, 2, 1, 2, 2, 4 ),
 ( 0.000000000000000000, 0.06252861023063965851, 0.07034468650946289203, 0.07425272464887451573, 0.07816076278828612556, 0.09379291534592466839, 0.1094250679035632251, 0.1172411441823824341, 0.1211491823217919622, 0.1231032013914969692, 0.1240802109263322434, 0.1250572204611674898, 0.1875858306902031536, 0.2188501358047209855, 0.2344822883619798459, 0.2422983646406044467, 0.2462064027799215904, 0.2501144409192387341, 0.3126430511484086794, 0.3439073562629967884, 0.3595395088202907319, 0.3673555850989377869, 0.3751716613775847864, 0.5002288818359376110 ),
 .UNSPECIFIED. ) ;
#3106=CARTESIAN_POINT ( 'NONE',  ( -245.8375576770692987, -9.148519943277513278, -7.766315674714080686 ) ) ;
#3111=CARTESIAN_POINT ( 'NONE',  ( -245.5963909203066748, 9.039317601246798617, -7.892311131080197661 ) ) ;
#3144=CARTESIAN_POINT ( 'NONE',  ( -239.0453880742558113, -1.263976212796292353, -11.93324491903367068 ) ) ;
#3170=CARTESIAN_POINT ( 'NONE',  ( -243.2722961584167649, -7.557668641858518832, -9.321309795594205028 ) ) ;
#3175=ORIENTED_EDGE ( 'NONE', *, *, #2036, .F. ) ;
#3177=CARTESIAN_POINT ( 'NONE',  ( -243.5050917946776963, 7.747614400781131394, -9.163721889595233705 ) ) ;
#3185=CARTESIAN_POINT ( 'NONE',  ( -229.9813066729109039, 11.63677616891658140, -2.954026154813843785 ) ) ;
#3196=FACE_OUTER_BOUND ( 'NONE', #6862, .T. ) ;
#3197=ADVANCED_FACE ( 'NONE', ( #10759 ), #4890, .T. ) ;
#3204=EDGE_CURVE ( 'NONE', #10691, #4229, #6359, .T. ) ;
#3226=FACE_OUTER_BOUND ( 'NONE', #9756, .T. ) ;
#3230=DIRECTION ( 'NONE',  ( 0.000000000000000000, 0.000000000000000000, -1.000000000000000000 ) ) ;
#3239=CARTESIAN_POINT ( 'NONE',  ( -245.3462090897166661, -8.922924798440801553, -8.026147512420349628 ) ) ;
#3243=CARTESIAN_POINT ( 'NONE',  ( -240.6982673021772712, 4.277714796599771496, -11.21297710698476102 ) ) ;
#3255=ORIENTED_EDGE ( 'NONE', *, *, #6938, .F. ) ;
#3268=EDGE_LOOP ( 'NONE', ( #4933, #11971, #5702, #8405, #11746, #4696 ) ) ;
#3293=CARTESIAN_POINT ( 'NONE',  ( -229.6889200636375108, 1.000000000000000000, -11.95826074310140008 ) ) ;
#3296=CARTESIAN_POINT ( 'NONE',  ( -246.2429388863588997, 9.313684383704458725, 7.566737218046005964 ) ) ;
#3308=B_SPLINE_CURVE_WITH_KNOTS ( 'NONE', 3,
 ( #8935, #5599, #5730, #3657, #6803, #6867, #9659, #9788, #3727, #7727, #12995, #669, #10731, #7793, #12722, #11863, #2711, #542, #8663, #1604, #10858, #740, #4790, #5665, #7861, #2653, #11929, #10928, #5373, #12503, #9445, #10062, #2911, #9064, #8384, #934, #317, #6381, #994, #6995, #4056, #3050, #242, #6004, #9997, #12059, #4300, #3986, #9124, #1, #7440, #11060, #10439, #10181, #5137, #12445, #8000, #4988, #6128, #4370, #3296, #3925, #9000, #5048, #865, #5932, #5306, #2298, #1059, #1309, #7377, #9377, #7065, #2983, #1931, #11440, #8450, #4926, #2056, #3354, #1997, #8061, #7134 ),
 .UNSPECIFIED., .F., .F.,
 ( 4, 2, 1, 1, 1, 2, 2, 2, 1, 1, 1, 1, 2, 2, 2, 2, 1, 1, 1, 1, 2, 2, 2, 2, 1, 1, 1, 2, 2, 2, 1, 1, 1, 1, 2, 2, 2, 2, 1, 1, 1, 2, 2, 2, 1, 1, 2, 2, 2, 1, 1, 2, 2, 4 ),
 ( 0.000000000000000000, 0.06250000000019761970, 0.09375000000029638791, 0.1093750000003448075, 0.1171875000003690104, 0.1210937500003811534, 0.1250000000003932965, 0.1875000000005736522, 0.2187500000006650791, 0.2343750000007107925, 0.2421875000007349399, 0.2460937500007456535, 0.2480468750007523426, 0.2500000000007590595, 0.3125000000009455770, 0.3437500000010404455, 0.3593750000010878520, 0.3671875000011132206, 0.3710937500011274870, 0.3730468750011329826, 0.3740234375011340928, 0.3750000000011352586, 0.4375000000010309531, 0.4687500000009787171, 0.4843750000009543477, 0.4921875000009404144, 0.4960937500009318657, 0.4980468750009276468, 0.5000000000009233725, 0.5625000000007391865, 0.5937500000006448175, 0.6093750000005976331, 0.6171875000005760947, 0.6210937500005654366, 0.6230468750005599965, 0.6250000000005546674, 0.6875000000004986012, 0.7187500000004706235, 0.7343750000004566347, 0.7421875000004468648, 0.7460937500004449774, 0.7480468750004409806, 0.7500000000004370948, 0.7812500000003682610, 0.7968750000003311795, 0.8046875000003151923, 0.8085937500003100853, 0.8125000000003048672, 0.8437500000002730038, 0.8593750000002597922, 0.8671875000002503553, 0.8710937500002429168, 0.8750000000002353673, 1.000000000000000000 ),
 .UNSPECIFIED. ) ;
#3310=CARTESIAN_POINT ( 'NONE',  ( -243.2557941819830489, 7.548840537005648166, -9.332172160760025648 ) ) ;
#3311=CARTESIAN_POINT ( 'NONE',  ( -239.6349225408002042, 1.943794467312871088, 11.84155609439077494 ) ) ;
#3315=CARTESIAN_POINT ( 'NONE',  ( -229.7893046524160070, 6.871240432487316419, -9.845066738254859118 ) ) ;
#3325=CARTESIAN_POINT ( 'NONE',  ( -246.3306884223085262, -9.347001913672279727, 7.525531261391552817 ) ) ;
#3331=CARTESIAN_POINT ( 'NONE',  ( -229.8944816512308194, -9.773716331048332151, 6.972390473299147295 ) ) ;
#3332=ORIENTED_EDGE ( 'NONE', *, *, #11735, .T. ) ;
#3354=CARTESIAN_POINT ( 'NONE',  ( -247.9076433804861779, 9.798874666929192401, 6.926911304954392001 ) ) ;
#3370=CARTESIAN_POINT ( 'NONE',  ( -242.7490684365845084, 7.085544791023568045, -9.685620088677287853 ) ) ;
#3421=CIRCLE ( 'NONE', #9153, 12.00000000000000000 ) ;
#3439=CARTESIAN_POINT ( 'NONE',  ( -244.1511139045946379, 8.221670796178244700, -8.740858669765747990 ) ) ;
#3447=CARTESIAN_POINT ( 'NONE',  ( -229.6921628766824313, 1.744838226299831874, 11.89597424155227401 ) ) ;
#3469=CARTESIAN_POINT ( 'NONE',  ( -241.2864786002215851, -5.310083909452205653, -10.76118394184675964 ) ) ;
#3471=CARTESIAN_POINT ( 'NONE',  ( -229.6921609078544577, -1.744386008313467240, 11.89601205791960936 ) ) ;
#3472=ORIENTED_EDGE ( 'NONE', *, *, #6143, .F. ) ;
#3510=CARTESIAN_POINT ( 'NONE',  ( -239.0270226278116752, 1.232440503845085411, 11.93654573081539816 ) ) ;
#3574=CARTESIAN_POINT ( 'NONE',  ( -245.7661201684729804, -9.116795906119264714, 7.802929254751410859 ) ) ;
#3578=CARTESIAN_POINT ( 'NONE',  ( -229.7805228887153817, 6.572088255991269001, 10.04733889956801107 ) ) ;
#3579=EDGE_CURVE ( 'NONE', #12119, #1218, #12254, .T. ) ;
#3595=DIRECTION ( 'NONE',  ( -1.000000000000000000, 0.000000000000000000, 0.000000000000000000 ) ) ;
#3632=DIRECTION ( 'NONE',  ( -1.000000000000000000, 0.000000000000000000, 0.000000000000000000 ) ) ;
#3642=CARTESIAN_POINT ( 'NONE',  ( -239.4371284390123265, -1.766671737021507038, 11.86923926939766538 ) ) ;
#3657=CARTESIAN_POINT ( 'NONE',  ( -240.2229988807279426, 3.132498172464299735, 11.58475653428652308 ) ) ;
#3666=CARTESIAN_POINT ( 'NONE',  ( -229.9855622942915829, -11.72012966610593132, 2.583340135804222726 ) ) ;
#3667=AXIS2_PLACEMENT_3D ( 'NONE', #4633, #1210, #12411 ) ;
#3695=CARTESIAN_POINT ( 'NONE',  ( -249.7604317440018917, 11.15122115093721789, -4.588451767843126028 ) ) ;
#3711=CARTESIAN_POINT ( 'NONE',  ( -249.7969288063775366, -11.93744875558342855, 1.454679372137933191 ) ) ;
#3713=CARTESIAN_POINT ( 'NONE',  ( -243.5376947841703270, -7.773445842367210368, 9.141748602850459093 ) ) ;
#3716=CARTESIAN_POINT ( 'NONE',  ( -229.8177839478270528, 7.761208678071466416, 9.154234884485560997 ) ) ;
#3727=CARTESIAN_POINT ( 'NONE',  ( -240.4767932493586784, 3.790394256715869492, 11.38565896274182521 ) ) ;
#3772=CARTESIAN_POINT ( 'NONE',  ( -242.6565957993711322, -6.994822106563381325, 9.751204008824640113 ) ) ;
#3776=LINE ( 'NONE', #12914, #12242 ) ;
#3799=CARTESIAN_POINT ( 'NONE',  ( -242.6194444000231840, -6.961689675190617876, -9.776526358366776748 ) ) ;
#3800=CARTESIAN_POINT ( 'NONE',  ( -229.9454081747827559, -10.90707088183632578, -5.058745115878076959 ) ) ;
#3816=CARTESIAN_POINT ( 'NONE',  ( -239.6374854870928175, -1.945441273133328375, 11.84125337029676395 ) ) ;
#3841=CARTESIAN_POINT ( 'NONE',  ( -243.8618317092116285, -8.020662184074483392, 8.926546576192178506 ) ) ;
#3842=CARTESIAN_POINT ( 'NONE',  ( -239.1349169580540206, 1.405155701076436392, -11.91743587425622586 ) ) ;
#3854=CYLINDRICAL_SURFACE ( 'NONE', #1513, 230.0000000000000000 ) ;
#3865=CARTESIAN_POINT ( 'NONE',  ( -229.7197800013692017, -3.900097070943512545, -11.35015525795997426 ) ) ;
#3892=CARTESIAN_POINT ( 'NONE',  ( -239.5448319055423099, -1.867756360462773602, -11.85375772759396718 ) ) ;
#3909=CARTESIAN_POINT ( 'NONE',  ( -242.3288872984456361, -6.653385920035336909, 9.986615906358528250 ) ) ;
#3922=CARTESIAN_POINT ( 'NONE',  ( -248.3022220570269099, 9.870789006252802977, -6.824104388866809145 ) ) ;
#3925=CARTESIAN_POINT ( 'NONE',  ( -246.2633612349185626, 9.321506464660762603, 7.557087659995063156 ) ) ;
#3931=CARTESIAN_POINT ( 'NONE',  ( -229.9710968621332654, -11.43322075889305189, -3.663687894926668687 ) ) ;
#3949=CARTESIAN_POINT ( 'NONE',  ( -239.0387908882599106, -1.252775419848246363, 11.93442892173632330 ) ) ;
#3952=ADVANCED_BREP_SHAPE_REPRESENTATION ( '', ( #10422, #805 ), #1657 ) ;
#3958=CARTESIAN_POINT ( 'NONE',  ( -238.6985546646470198, 6.516754929249349828E-09, -12.00000000011316459 ) ) ;
#3961=B_SPLINE_CURVE_WITH_KNOTS ( 'NONE', 3,
 ( #11679, #7668, #11744, #6685, #1541, #5809, #4795, #2596, #12606, #10738, #9665, #8805, #2536, #5608, #547, #9796, #1609, #609, #3469, #4728, #8670, #12869, #11815, #7544, #2471, #6548, #7799, #11871, #2719, #6810, #10601, #10868, #5040, #3799, #12385, #2112, #5175, #3170, #1120, #7253, #2974, #4245, #11243, #8126, #10243, #4178, #8324, #9186, #10374, #2249, #11938, #8195, #12256, #11115, #3239, #12314, #3106, #7183, #1985, #7320, #11319, #7055, #1248, #5108, #62, #6059, #12932, #4115, #6324, #11387, #12186, #10113, #6262, #9254, #459, #6189, #9114, #8869, #10171, #985, #129, #1050, #7866 ),
 .UNSPECIFIED., .F., .F.,
 ( 4, 2, 1, 1, 1, 2, 2, 2, 1, 1, 1, 1, 2, 2, 2, 2, 1, 1, 1, 1, 2, 2, 2, 2, 1, 1, 1, 2, 2, 2, 1, 1, 1, 1, 2, 2, 2, 2, 1, 1, 1, 2, 2, 2, 1, 1, 2, 2, 2, 1, 1, 2, 2, 4 ),
 ( 0.000000000000000000, 0.06250000000013644641, 0.09375000000020380919, 0.1093750000002384343, 0.1171875000002566974, 0.1210937500002668976, 0.1250000000002770839, 0.1875000000004268808, 0.2187500000005017098, 0.2343750000005390688, 0.2421875000005577483, 0.2460937500005684342, 0.2480468750005739020, 0.2500000000005793699, 0.3125000000007500667, 0.3437500000008369416, 0.3593750000008821277, 0.3671875000009031109, 0.3710937500009120482, 0.3730468750009181544, 0.3740234375009196532, 0.3750000000009210965, 0.4375000000009141021, 0.4687500000009104939, 0.4843750000009103274, 0.4921875000009120482, 0.4960937500009112155, 0.4980468750009108270, 0.5000000000009103829, 0.5625000000007968071, 0.5937500000007399636, 0.6093750000007095435, 0.6171875000006963319, 0.6210937500006896705, 0.6230468750006864509, 0.6250000000006831202, 0.6875000000006470380, 0.7187500000006311618, 0.7343750000006259437, 0.7421875000006260548, 0.7460937500006262768, 0.7480468750006264989, 0.7500000000006266099, 0.7812500000005730971, 0.7968750000005464518, 0.8046875000005330181, 0.8085937500005236922, 0.8125000000005143663, 0.8437500000004438672, 0.8593750000004061196, 0.8671875000003899103, 0.8710937500003791412, 0.8750000000003683720, 1.000000000000000000 ),
 .UNSPECIFIED. ) ;
#3971=CARTESIAN_POINT ( 'NONE',  ( -240.5058532487308582, -3.857938722311311075, 11.36295048183375300 ) ) ;
#3972=CARTESIAN_POINT ( 'NONE',  ( -239.4909294952468315, 1.818763105859342755, -11.86135880463733727 ) ) ;
#3986=CARTESIAN_POINT ( 'NONE',  ( -244.6090102851887593, 8.514624253206315885, 8.455955369777946373 ) ) ;
#4007=CARTESIAN_POINT ( 'NONE',  ( -239.4329164336750466, -1.762478856070534006, 11.86986396151673517 ) ) ;
#4021=CARTESIAN_POINT ( 'NONE',  ( -239.0745754881768050, -1.312373183774685703, -11.92802719768877573 ) ) ;
#4041=CARTESIAN_POINT ( 'NONE',  ( -239.4341775791918394, 1.763735210516577778, -11.86967692145091213 ) ) ;
#4052=CARTESIAN_POINT ( 'NONE',  ( -247.0023889698559287, 9.573823397979071004, -7.235426327079722775 ) ) ;
#4056=CARTESIAN_POINT ( 'NONE',  ( -243.4562500152165399, 7.708554438554969579, 9.196640587735709360 ) ) ;
#4088=CARTESIAN_POINT ( 'NONE',  ( -239.4798992437278855, -1.808255580866046985, -11.86296839994171926 ) ) ;
#4115=CARTESIAN_POINT ( 'NONE',  ( -246.8626574249385328, -9.530421748743428623, -7.291787928471770819 ) ) ;
#4121=CARTESIAN_POINT ( 'NONE',  ( -246.5457465964734638, 9.425397934458551674, -7.427386667154282307 ) ) ;
#4138=CARTESIAN_POINT ( 'NONE',  ( 0.000000000000000000, -2.156506209390995021, 0.000000000000000000 ) ) ;
#4154=CARTESIAN_POINT ( 'NONE',  ( -238.7337772397934259, -0.4297369727470538581, -11.99275889149802055 ) ) ;
#4165=ORIENTED_EDGE ( 'NONE', *, *, #11572, .F. ) ;
#4178=CARTESIAN_POINT ( 'NONE',  ( -244.2419534911824144, -8.283406880650625581, -8.682674419792185461 ) ) ;
#4181=ADVANCED_FACE ( 'NONE', ( #12885 ), #5013, .T. ) ;
#4184=CARTESIAN_POINT ( 'NONE',  ( -245.1341653173766701, 8.810613775113198542, -8.147076446705556307 ) ) ;
#4196=EDGE_CURVE ( 'NONE', #11418, #6137, #3093, .T. ) ;
#4200=CARTESIAN_POINT ( 'NONE',  ( -248.8841473305942031, -9.947364712437689604, 6.711964937432249201 ) ) ;
#4229=VERTEX_POINT ( 'NONE', #8229 ) ;
#4245=CARTESIAN_POINT ( 'NONE',  ( -243.4720072945285096, -7.721209753983143464, -9.186020676454910827 ) ) ;
#4251=CARTESIAN_POINT ( 'NONE',  ( -244.7207088138438280, 8.581273372657582499, -8.388577724893742982 ) ) ;
#4268=CARTESIAN_POINT ( 'NONE',  ( -247.4131856421704470, -9.690266168923910683, 7.079595845687837397 ) ) ;
#4300=CARTESIAN_POINT ( 'NONE',  ( -244.4094253640295449, 8.392574418407512837, 8.577616032622085385 ) ) ;
#4315=CARTESIAN_POINT ( 'NONE',  ( -239.4459774607273346, 1.775548040146878614, 11.86792666930613116 ) ) ;
#4321=CARTESIAN_POINT ( 'NONE',  ( -229.7549662686524243, 5.608571857102900182, -10.61518803634819008 ) ) ;
#4326=ORIENTED_EDGE ( 'NONE', *, *, #10291, .F. ) ;
#4333=CARTESIAN_POINT ( 'NONE',  ( -246.3021867260266333, -9.336273485124390703, 7.538834026449642067 ) ) ;
#4340=SHAPE_REPRESENTATION ( 'Drain Plug', ( #805 ), #1657 ) ;
#4370=CARTESIAN_POINT ( 'NONE',  ( -246.1949466625434866, 9.295128601630475274, 7.589564689875960113 ) ) ;
#4373=DIRECTION ( 'NONE',  ( 0.000000000000000000, -1.000000000000000000, 0.000000000000000000 ) ) ;
#4374=CIRCLE ( 'NONE', #7359, 249.7999999999999829 ) ;
#4382=CARTESIAN_POINT ( 'NONE',  ( -243.5834864928935417, 7.809424032089159695, -9.110990436254303049 ) ) ;
#4414=ADVANCED_FACE ( 'NONE', ( #8482 ), #6550, .F. ) ;
#4426=( LENGTH_UNIT ( ) NAMED_UNIT ( * ) SI_UNIT ( .MILLI., .METRE. ) );
#4437=EDGE_CURVE ( 'NONE', #12119, #1218, #5796, .T. ) ;
#4440=CARTESIAN_POINT ( 'NONE',  ( -243.6755871756574550, 7.880721788829606389, -9.049489450626314380 ) ) ;
#4447=CARTESIAN_POINT ( 'NONE',  ( -229.8175486381514361, 7.757877409022798432, -9.162773420015767556 ) ) ;
#4481=EDGE_CURVE ( 'NONE', #12785, #12119, #6812, .T. ) ;
#4487=EDGE_CURVE ( 'NONE', #5558, #10691, #3308, .T. ) ;
#4492=( NAMED_UNIT ( * ) SI_UNIT ( $, .STERADIAN. ) SOLID_ANGLE_UNIT ( ) );
#4504=CARTESIAN_POINT ( 'NONE',  ( -238.7054577249708132, 0.2141779464642266373, 11.99854502510401666 ) ) ;
#4569=CARTESIAN_POINT ( 'NONE',  ( -239.4297296705752558, 1.759293724106229861, 11.87033638227847909 ) ) ;
#4571=DIRECTION ( 'NONE',  ( 1.000000000000000000, 0.000000000000000000, 0.000000000000000000 ) ) ;
#4573=DIRECTION ( 'NONE',  ( 0.000000000000000000, -1.000000000000000000, 0.000000000000000000 ) ) ;
#4576=CARTESIAN_POINT ( 'NONE',  ( -229.9447701116965277, 10.89162700641532666, 5.050967065786899468 ) ) ;
#4587=DIRECTION ( 'NONE',  ( 1.000000000000000000, 0.000000000000000000, 0.000000000000000000 ) ) ;
#4629=CARTESIAN_POINT ( 'NONE',  ( -249.7999494874248398, -11.99892863383222874, -1.190337990051804296 ) ) ;
#4633=CARTESIAN_POINT ( 'NONE',  ( 0.000000000000000000, 0.000000000000000000, 0.000000000000000000 ) ) ;
#4647=DIRECTION ( 'NONE',  ( 0.000000000000000000, -1.000000000000000000, 0.000000000000000000 ) ) ;
#4660=CARTESIAN_POINT ( 'NONE',  ( -229.7627910449494664, -5.948779906797049932, 10.44832732976153800 ) ) ;
#4696=ORIENTED_EDGE ( 'NONE', *, *, #6394, .F. ) ;
#4703=CARTESIAN_POINT ( 'NONE',  ( -245.5556485997495031, -9.020247694314779352, 7.914083889440647113 ) ) ;
#4708=CARTESIAN_POINT ( 'NONE',  ( -229.6889200636375108, 1.000000000000000000, 11.95826074310140008 ) ) ;
#4728=CARTESIAN_POINT ( 'NONE',  ( -241.2922373264150906, -5.318940986358126288, -10.75680814014601872 ) ) ;
#4729=CARTESIAN_POINT ( 'NONE',  ( -229.9954967225296514, -11.91353440303754319, -1.485748047147350537 ) ) ;
#4730=AXIS2_PLACEMENT_3D ( 'NONE', #7277, #4571, #8349 ) ;
#4774=CARTESIAN_POINT ( 'NONE',  ( -244.8469727609692370, -8.653369516671046924, 8.313800303729999897 ) ) ;
#4775=CARTESIAN_POINT ( 'NONE',  ( -238.9270525397529070, 1.044268037043195374, -11.95485691270613593 ) ) ;
#4777=EDGE_LOOP ( 'NONE', ( #9900, #2953, #10450, #6156 ) ) ;
#4778=CARTESIAN_POINT ( 'NONE',  ( -229.9988754446348196, 11.97852054161528024, -0.7430525309543891677 ) ) ;
#4790=CARTESIAN_POINT ( 'NONE',  ( -241.8394219714712108, 6.081466911235927419, 10.34544425800572398 ) ) ;
#4795=CARTESIAN_POINT ( 'NONE',  ( -240.4404613007271507, -3.704209566672288290, -11.41407139955809669 ) ) ;
#4798=CARTESIAN_POINT ( 'NONE',  ( -229.9999900080290729, -11.99981304996879850, -0.3780019861745291809 ) ) ;
#4810=CARTESIAN_POINT ( 'NONE',  ( -239.6697886840235583, -1.970929121827114106, 11.83704280384634266 ) ) ;
#4827=AXIS2_PLACEMENT_3D ( 'NONE', #933, #9061, #10927 ) ;
#4834=CARTESIAN_POINT ( 'NONE',  ( -242.3253012572137948, -6.649486011330081325, 9.989214338957303596 ) ) ;
#4838=CARTESIAN_POINT ( 'NONE',  ( -239.0407087265602399, 1.256038988924583988, -11.93408471340098664 ) ) ;
#4867=CARTESIAN_POINT ( 'NONE',  ( -229.7804030572558247, -6.567824493990499057, -10.05005982919573881 ) ) ;
#4869=ORIENTED_EDGE ( 'NONE', *, *, #12723, .T. ) ;
#4882=UNCERTAINTY_MEASURE_WITH_UNIT (LENGTH_MEASURE( 1.000000000000000082E-05 ), #2562, 'distance_accuracy_value', 'NONE');
#4884=CARTESIAN_POINT ( 'NONE',  ( -239.4330563949805537, -1.762617345644425404, 11.86984317963793778 ) ) ;
#4886=VERTEX_POINT ( 'NONE', #5330 ) ;
#4890=CYLINDRICAL_SURFACE ( 'NONE', #10713, 249.7999999999999829 ) ;
#4892=CARTESIAN_POINT ( 'NONE',  ( -239.8750565963660506, -2.115697797198144769, -11.81209311402866646 ) ) ;
#4908=CARTESIAN_POINT ( 'NONE',  ( -242.5248711350201631, -6.860954764109954418, 9.845341014195845730 ) ) ;
#4912=DIRECTION ( 'NONE',  ( 0.000000000000000000, 0.000000000000000000, 1.000000000000000000 ) ) ;
#4926=CARTESIAN_POINT ( 'NONE',  ( -247.8580199589107451, 9.788721918689880397, 6.941247868350859385 ) ) ;
#4931=CARTESIAN_POINT ( 'NONE',  ( -229.6921463704719883, -1.741046932630716526, -11.89629128545617043 ) ) ;
#4933=ORIENTED_EDGE ( 'NONE', *, *, #12510, .F. ) ;
#4947=CARTESIAN_POINT ( 'NONE',  ( -239.0463147773640742, -1.265540211687415484, 11.93307915096743166 ) ) ;
#4948=VERTEX_POINT ( 'NONE', #7919 ) ;
#4961=AXIS2_PLACEMENT_3D ( 'NONE', #11314, #4373, #1186 ) ;
#4974=CARTESIAN_POINT ( 'NONE',  ( -240.5255509705923771, -3.902938849136275756, 11.34756747380466990 ) ) ;
#4975=CARTESIAN_POINT ( 'NONE',  ( -239.6374854881607348, 1.945441273982636776, -11.84125337015805179 ) ) ;
#4985=CARTESIAN_POINT ( 'NONE',  ( -247.4131856387215862, 9.690266168050630569, -7.079595847188384639 ) ) ;
#4988=CARTESIAN_POINT ( 'NONE',  ( -246.0119047653037114, 9.221725595239210094, 7.678802607589900298 ) ) ;
#4997=CARTESIAN_POINT ( 'NONE',  ( -229.9968630190249712, -11.93995442319631373, 1.297703334126907304 ) ) ;
#5013=PLANE ( 'NONE',  #8288 ) ;
#5021=CARTESIAN_POINT ( 'NONE',  ( -238.8644114632761557, -0.8921807392855528596, -11.96685057743542480 ) ) ;
#5035=CARTESIAN_POINT ( 'NONE',  ( -239.6107305625394872, 1.923727078433295601, -11.84479882075283541 ) ) ;
#5040=CARTESIAN_POINT ( 'NONE',  ( -242.4509935382772596, -6.787150506045976250, -9.898021028433552360 ) ) ;
#5048=CARTESIAN_POINT ( 'NONE',  ( -246.2818250957199098, 9.328552628620979448, 7.548386157364489257 ) ) ;
#5066=CARTESIAN_POINT ( 'NONE',  ( -233.0000000000000000, 1.000000000000000000, -12.50000000000000000 ) ) ;
#5083=CARTESIAN_POINT ( 'NONE',  ( -239.4571233178585317, -1.786328300567973315, -11.86629109653343050 ) ) ;
#5108=CARTESIAN_POINT ( 'NONE',  ( -246.2818250957594159, -9.328552628636005650, -7.548386157348565995 ) ) ;
#5129=EDGE_CURVE ( 'NONE', #644, #8290, #2876, .T. ) ;
#5137=CARTESIAN_POINT ( 'NONE',  ( -245.3462090940810754, 8.922924800614550733, 8.026147510179294287 ) ) ;
#5175=CARTESIAN_POINT ( 'NONE',  ( -243.1855895750504430, -7.483404893957491311, -9.380758043683870895 ) ) ;
#5181=CARTESIAN_POINT ( 'NONE',  ( -240.7937243741888551, 4.465328606765308628, -11.13898957095615572 ) ) ;
#5187=B_SPLINE_CURVE_WITH_KNOTS ( 'NONE', 3,
 ( #2447, #1324, #4504, #258, #12708, #11593, #7582, #7520, #9458, #9391, #1257, #10520, #6329, #10379, #8590, #2508, #7326, #3510, #8464, #7454, #12518, #12648, #10646, #9514, #6525, #6590, #2384, #9636, #523, #5321, #4569, #4315, #8652, #12458, #5452, #3311, #10453, #5390, #7389, #330 ),
 .UNSPECIFIED., .F., .F.,
 ( 4, 2, 1, 1, 2, 2, 2, 2, 1, 1, 2, 2, 2, 2, 1, 1, 1, 1, 2, 2, 2, 2, 2, 4 ),
 ( 0.5002288818359376110, 0.5627002716060051091, 0.5939359664910388581, 0.6095538139335572314, 0.6173627376548146417, 0.6251716613760720520, 0.6876430511461220085, 0.7188787460311498734, 0.7344965934736605861, 0.7423055171949158870, 0.7462099790555436485, 0.7501144409161712989, 0.8125858306861062363, 0.8438215255710737051, 0.8594393730135573284, 0.8672482967347945326, 0.8711527585954177422, 0.8731049895257294580, 0.8740811049908898678, 0.8750572204560502776, 0.9062929153420298256, 0.9219107627850194886, 0.9375286102280091516, 1.000000000000000000 ),
 .UNSPECIFIED. ) ;
#5188=CARTESIAN_POINT ( 'NONE',  ( -229.9710174714563209, 11.43162843135961459, -3.668625443667830499 ) ) ;
#5251=CARTESIAN_POINT ( 'NONE',  ( -241.3126941818516400, 5.350247869163432313, -10.74127079069710788 ) ) ;
#5270=CARTESIAN_POINT ( 'NONE',  ( -247.9529057712887834, -9.807895051005736775, 6.914131050820655489 ) ) ;
#5306=CARTESIAN_POINT ( 'NONE',  ( -246.7640704956085926, 9.498771479817998298, 7.332983348267928747 ) ) ;
#5320=CARTESIAN_POINT ( 'NONE',  ( -244.8469727607960351, 8.653369516572549713, -8.313800303827326488 ) ) ;
#5321=CARTESIAN_POINT ( 'NONE',  ( -239.4273512216421409, 1.756910838264598596, 11.87068934081676019 ) ) ;
#5330=CARTESIAN_POINT ( 'NONE',  ( -239.9450917581424960, 2.156506209390990136, -11.80463811257499884 ) ) ;
#5340=CARTESIAN_POINT ( 'NONE',  ( -246.3576883206671653, -9.357104192533332920, 7.512982112701342530 ) ) ;
#5373=CARTESIAN_POINT ( 'NONE',  ( -242.2842939341516626, 6.604577240802537830, 10.01896504304081326 ) ) ;
#5389=CARTESIAN_POINT ( 'NONE',  ( -241.3214569866001398, 5.363580936733816529, -10.73461844913050101 ) ) ;
#5390=CARTESIAN_POINT ( 'NONE',  ( -239.7865846207793936, 2.059993156293506544, 11.82215868828261129 ) ) ;
#5397=CIRCLE ( 'NONE', #4961, 249.7999999999999829 ) ;
#5416=CARTESIAN_POINT ( 'NONE',  ( -229.9448021440930461, -10.89127638036671719, 5.041528041963096562 ) ) ;
#5451=CARTESIAN_POINT ( 'NONE',  ( -244.4430806157185430, 8.412306931070002491, -8.557769321120538564 ) ) ;
#5452=CARTESIAN_POINT ( 'NONE',  ( -239.5718914762306611, 1.891487839302555374, 11.85001484810088535 ) ) ;
#5455=CARTESIAN_POINT ( 'NONE',  ( 0.000000000000000000, 9.997999799959989886, 0.000000000000000000 ) ) ;
#5457=CARTESIAN_POINT ( 'NONE',  ( -229.7326367665251894, 4.595192083928767879, -11.08697888960004896 ) ) ;
#5497=B_SPLINE_CURVE_WITH_KNOTS ( 'NONE', 3,
 ( #8846, #1783, #7707, #11721, #4629, #5851, #3711, #10841, #8977, #12774, #6918, #6846, #6783 ),
 .UNSPECIFIED., .F., .F.,
 ( 4, 2, 2, 1, 2, 2, 4 ),
 ( 0.000000000000000000, 0.2500000000000000555, 0.5000000000000001110, 0.6250000000000001110, 0.6875000000000000000, 0.7499999999999998890, 1.000000000000000000 ),
 .UNSPECIFIED. ) ;
#5518=VECTOR ( 'NONE', #11018, 1000.000000000000000 ) ;
#5520=CARTESIAN_POINT ( 'NONE',  ( -239.9450917581424960, 2.156506209390990136, -11.80463811257499884 ) ) ;
#5522=CARTESIAN_POINT ( 'NONE',  ( -229.8898327533349573, 9.665891927765104086, 7.128580859766620925 ) ) ;
#5538=CARTESIAN_POINT ( 'NONE',  ( -229.7320401093896578, -4.610569389177691768, 11.10393803714480754 ) ) ;
#5558=VERTEX_POINT ( 'NONE', #488 ) ;
#5581=CARTESIAN_POINT ( 'NONE',  ( -249.5626403297915772, -9.995018771280594905, 6.640755139178303956 ) ) ;
#5587=CARTESIAN_POINT ( 'NONE',  ( -229.9651316831089787, 11.31282158159266693, 4.019724534361353463 ) ) ;
#5598=CARTESIAN_POINT ( 'NONE',  ( -250.0000000000000000, 0.000000000000000000, -12.00000000000000000 ) ) ;
#5599=CARTESIAN_POINT ( 'NONE',  ( -240.0092717900960793, 2.435426587042586188, 11.75368411291894688 ) ) ;
#5608=CARTESIAN_POINT ( 'NONE',  ( -241.0259582380425911, -4.889855348568320714, -10.95996151980668643 ) ) ;
#5609=CARTESIAN_POINT ( 'NONE',  ( -229.8758510084904572, -9.325226166226105562, 7.561748853445185325 ) ) ;
#5635=( NAMED_UNIT ( * ) SI_UNIT ( $, .STERADIAN. ) SOLID_ANGLE_UNIT ( ) );
#5636=PRESENTATION_STYLE_ASSIGNMENT (( #444 ) ) ;
#5665=CARTESIAN_POINT ( 'NONE',  ( -241.9271341497538970, 6.190796898938002002, 10.28045873024532320 ) ) ;
#5689=ORIENTED_EDGE ( 'NONE', *, *, #5737, .T. ) ;
#5702=ORIENTED_EDGE ( 'NONE', *, *, #9422, .F. ) ;
#5712=CARTESIAN_POINT ( 'NONE',  ( -242.3537289171788132, -6.680330752951019413, 9.968624626860709270 ) ) ;
#5730=CARTESIAN_POINT ( 'NONE',  ( -240.0865915474595624, 2.714760371449491227, 11.69235895546072790 ) ) ;
#5737=EDGE_CURVE ( 'NONE', #6137, #8105, #8074, .T. ) ;
#5741=CARTESIAN_POINT ( 'NONE',  ( -229.7396143013220637, -4.939964479293777799, -10.94242647241850186 ) ) ;
#5744=CIRCLE ( 'NONE', #1489, 240.2352941176469869 ) ;
#5757=CARTESIAN_POINT ( 'NONE',  ( -238.9270525380257197, -1.044268033339604829, 11.95485691302340037 ) ) ;
#5778=DIRECTION ( 'NONE',  ( 0.000000000000000000, -1.000000000000000000, 0.000000000000000000 ) ) ;
#5783=CARTESIAN_POINT ( 'NONE',  ( -243.5050917946769857, -7.747614400781110966, 9.163721889611487370 ) ) ;
#5785=CARTESIAN_POINT ( 'NONE',  ( -239.6697886797803960, 1.970929118521804968, -11.83704280435266298 ) ) ;
#5788=CARTESIAN_POINT ( 'NONE',  ( -229.6989731110666924, 2.477381075173155978, 11.76526715247366894 ) ) ;
#5796=B_SPLINE_CURVE_WITH_KNOTS ( 'NONE', 3,
 ( #12607, #3471, #9726, #7546, #5538, #4660, #12675, #7669, #8740, #7606, #7482, #6615, #5609, #3331, #11484, #10481, #1350, #5416, #9480, #12542, #2789, #6009, #11816, #3666, #2856, #9822, #4997, #9007, #748, #8870, #4798, #11940, #4729, #1936, #806, #6875, #3931, #12934, #3800, #7867, #10937, #8806, #7737, #1813, #5877, #9931, #1671, #4867, #12870, #10066, #5741, #8007, #2661, #3865, #2720, #7800, #11874, #4931, #5810 ),
 .UNSPECIFIED., .F., .F.,
 ( 4, 2, 2, 2, 2, 2, 2, 2, 1, 2, 2, 1, 2, 2, 1, 2, 2, 2, 2, 2, 2, 2, 2, 2, 2, 2, 2, 2, 2, 2, 4 ),
 ( 0.000000000000000000, 0.06249999999999980571, 0.1249999999999996669, 0.1874999999999995282, 0.2187499999999995282, 0.2499999999999995559, 0.2812499999999995559, 0.3124999999999995559, 0.3437499999999996114, 0.3593749999999996114, 0.3749999999999996114, 0.4062499999999996114, 0.4218749999999996114, 0.4374999999999996114, 0.4687499999999997224, 0.4843749999999997780, 0.4999999999999997780, 0.5312499999999997780, 0.5624999999999997780, 0.5937499999999997780, 0.6249999999999997780, 0.6875000000000000000, 0.7500000000000001110, 0.7812500000000002220, 0.8125000000000002220, 0.8437500000000002220, 0.8750000000000002220, 0.9062500000000003331, 0.9218750000000002220, 0.9375000000000002220, 1.000000000000000000 ),
 .UNSPECIFIED. ) ;
#5805=VECTOR ( 'NONE', #7937, 1000.000000000000000 ) ;
#5809=CARTESIAN_POINT ( 'NONE',  ( -240.3908911751984760, -3.583360156735717617, -11.45287536844211473 ) ) ;
#5810=CARTESIAN_POINT ( 'NONE',  ( -229.6889200636375108, -1.000000000000000000, -11.95826074310140008 ) ) ;
#5826=CARTESIAN_POINT ( 'NONE',  ( -239.9450917581429792, -2.156506209390995021, 11.80463811257499884 ) ) ;
#5832=CARTESIAN_POINT ( 'NONE',  ( -250.0000000000000000, 1.000000000000000000, 11.95826074310140008 ) ) ;
#5851=CARTESIAN_POINT ( 'NONE',  ( -249.8000249158748716, -12.00052859682465112, 0.5791969794071849531 ) ) ;
#5854=CARTESIAN_POINT ( 'NONE',  ( -242.4607547069787188, -6.794574167113599295, 9.891349723532682603 ) ) ;
#5855=CARTESIAN_POINT ( 'NONE',  ( -239.0946434567509300, 1.343932711761059329, -11.92448114280328575 ) ) ;
#5877=CARTESIAN_POINT ( 'NONE',  ( -229.8176334827029734, -7.760374230956414543, -9.160644146514997033 ) ) ;
#5892=CARTESIAN_POINT ( 'NONE',  ( -239.6107305401175154, -1.923727060014592372, 11.84479882370300352 ) ) ;
#5913=FACE_OUTER_BOUND ( 'NONE', #4777, .T. ) ;
#5916=CARTESIAN_POINT ( 'NONE',  ( -240.5954930648636036, -4.058997395512141004, 11.29299565151879570 ) ) ;
#5918=CARTESIAN_POINT ( 'NONE',  ( -239.5355864646326154, 1.859542262448960148, -11.85503689126069915 ) ) ;
#5924=ORIENTED_EDGE ( 'NONE', *, *, #1182, .F. ) ;
#5931=CARTESIAN_POINT ( 'NONE',  ( -233.0000000000000000, -1.000000000000000000, 11.95826074310140008 ) ) ;
#5932=CARTESIAN_POINT ( 'NONE',  ( -246.5647187084086625, 9.432500522705552726, 7.418392397108976688 ) ) ;
#5960=CARTESIAN_POINT ( 'NONE',  ( -239.1644449915108908, -1.447449310967494629, 11.91236063150040003 ) ) ;
#5963=PRODUCT_DEFINITION_CONTEXT ( 'detailed design', #8893, 'design' ) ;
#5970=CARTESIAN_POINT ( 'NONE',  ( -238.7877125588677529, -0.6581212608206794545, -11.98194713172116543 ) ) ;
#5985=CARTESIAN_POINT ( 'NONE',  ( -244.8752249710313436, -8.669362157865133867, 8.297136228535620717 ) ) ;
#5986=CARTESIAN_POINT ( 'NONE',  ( -239.6279820821901296, 1.937806669454118946, -11.84250614158974280 ) ) ;
#5998=CARTESIAN_POINT ( 'NONE',  ( -246.1739743501388773, 9.287690275995652556, -7.598953578997135416 ) ) ;
#6004=CARTESIAN_POINT ( 'NONE',  ( -243.6963328790136245, 7.900314958675304311, 9.035065364342628413 ) ) ;
#6009=CARTESIAN_POINT ( 'NONE',  ( -229.9741363928493172, -11.49453502056800858, 3.481240219726035701 ) ) ;
#6025=CARTESIAN_POINT ( 'NONE',  ( -239.5624944382587103, -1.883403856151246947, 11.85129291893081138 ) ) ;
#6026=EDGE_LOOP ( 'NONE', ( #9311, #6688, #9986, #2969 ) ) ;
#6033=AXIS2_PLACEMENT_3D ( 'NONE', #1838, #10766, #8696 ) ;
#6036=CARTESIAN_POINT ( 'NONE',  ( -238.8086796927654802, -0.7305208660282929145, -11.97777837065560114 ) ) ;
#6051=CARTESIAN_POINT ( 'NONE',  ( -233.0000000000000000, 1.469576158976823947E-15, 12.00000000000000000 ) ) ;
#6054=CARTESIAN_POINT ( 'NONE',  ( -239.4529136937619000, 1.782225492116373600, -11.86690533460318342 ) ) ;
#6059=CARTESIAN_POINT ( 'NONE',  ( -246.5647187074482645, -9.432500522371258356, -7.418392397481870404 ) ) ;
#6065=CARTESIAN_POINT ( 'NONE',  ( -247.9423986615486797, 9.805815554877437279, -6.917079555552443360 ) ) ;
#6068=CARTESIAN_POINT ( 'NONE',  ( -249.7118339206215012, 9.997999799959989886, 6.636264009214830395 ) ) ;
#6098=CARTESIAN_POINT ( 'NONE',  ( -239.3382408973351119, -1.667768204462165116, -11.88390510034685299 ) ) ;
#6123=CARTESIAN_POINT ( 'NONE',  ( -245.8615520219217672, 9.158310437450982278, -7.754087231807664793 ) ) ;
#6128=CARTESIAN_POINT ( 'NONE',  ( -246.0976122680899607, 9.256780778463358672, 7.636466317080543575 ) ) ;
#6137=VERTEX_POINT ( 'NONE', #6728 ) ;
#6143=EDGE_CURVE ( 'NONE', #10691, #4229, #4374, .T. ) ;
#6156=ORIENTED_EDGE ( 'NONE', *, *, #12278, .F. ) ;
#6186=DIRECTION ( 'NONE',  ( 0.000000000000000000, -1.000000000000000000, 0.000000000000000000 ) ) ;
#6189=CARTESIAN_POINT ( 'NONE',  ( -247.6855308000310743, -9.751870871334467950, -6.992977238237519266 ) ) ;
#6194=CARTESIAN_POINT ( 'NONE',  ( -243.0412680634588583, 7.360923497056134579, -9.480357583680490308 ) ) ;
#6227=EDGE_CURVE ( 'NONE', #4886, #12985, #7542, .T. ) ;
#6233=CARTESIAN_POINT ( 'NONE',  ( -239.4988366478256125, -1.826140896386560186, -11.86023454918143472 ) ) ;
#6242=ORIENTED_EDGE ( 'NONE', *, *, #1586, .F. ) ;
#6252=CIRCLE ( 'NONE', #503, 12.00000000000000000 ) ;
#6262=CARTESIAN_POINT ( 'NONE',  ( -247.2298618823421066, -9.638957510065514711, -7.147826786427922130 ) ) ;
#6267=CARTESIAN_POINT ( 'NONE',  ( -244.8216528713956563, 8.638952368661110270, -8.328775923151233940 ) ) ;
#6284=CARTESIAN_POINT ( 'NONE',  ( -248.0636855464110795, -9.829232304199436498, 6.883789224096078740 ) ) ;
#6295=VERTEX_POINT ( 'NONE', #12554 ) ;
#6313=CARTESIAN_POINT ( 'NONE',  ( -250.0000000000000000, 1.000000000000000000, -11.95826074310140008 ) ) ;
#6324=CARTESIAN_POINT ( 'NONE',  ( -246.9756885463878859, -9.564884954983938314, -7.246373649491316016 ) ) ;
#6328=CARTESIAN_POINT ( 'NONE',  ( -244.1910629329458970, 8.248580893023101268, -8.715491049894939835 ) ) ;
#6329=CARTESIAN_POINT ( 'NONE',  ( -238.9284634072548670, 1.043171514628518537, 11.95464273948973322 ) ) ;
#6333=PRODUCT_CONTEXT ( 'NONE', #13001, 'mechanical' ) ;
#6338=TOROIDAL_SURFACE ( 'NONE', #585, 241.5000000000000000, 2.500000000000000000 ) ;
#6345=CARTESIAN_POINT ( 'NONE',  ( -246.8633775110742476, -9.531357831541830805, 7.291317142722177458 ) ) ;
#6359=B_SPLINE_CURVE_WITH_KNOTS ( 'NONE', 3,
 ( #6068, #12197, #12128, #1867, #11125, #10123, #11191, #10465, #11643, #2498, #3695, #11774, #11512 ),
 .UNSPECIFIED., .F., .F.,
 ( 4, 2, 2, 1, 2, 2, 4 ),
 ( 0.000000000000000000, 0.2500000000000000000, 0.4999999999999999445, 0.6250000000000000000, 0.6875000000000000000, 0.7500000000000000000, 1.000000000000000000 ),
 .UNSPECIFIED. ) ;
#6381=CARTESIAN_POINT ( 'NONE',  ( -243.2722961588427495, 7.557668642214872889, 9.321309795288598821 ) ) ;
#6394=EDGE_CURVE ( 'NONE', #7801, #4948, #7778, .T. ) ;
#6395=CARTESIAN_POINT ( 'NONE',  ( -242.3889174921309291, 6.718220501240577569, -9.943174754796373804 ) ) ;
#6399=PRODUCT ( 'Drain Plug', 'Drain Plug', '', ( #6333 ) ) ;
#6401=CARTESIAN_POINT ( 'NONE',  ( -229.6905319492641979, 1.370232268880117621, -11.92730036543203909 ) ) ;
#6419=CARTESIAN_POINT ( 'NONE',  ( -240.5118714936808999, -3.871746541839889755, 11.35824976270681574 ) ) ;
#6468=CARTESIAN_POINT ( 'NONE',  ( -229.7195872777370198, 3.900365664305255997, -11.35467465479823268 ) ) ;
#6516=( NAMED_UNIT ( * ) PLANE_ANGLE_UNIT ( ) SI_UNIT ( $, .RADIAN. ) );
#6523=DIRECTION ( 'NONE',  ( 0.000000000000000000, 0.000000000000000000, 1.000000000000000000 ) ) ;
#6525=CARTESIAN_POINT ( 'NONE',  ( -239.3529291969095425, 1.679452495051852789, 11.88190773406936884 ) ) ;
#6530=CARTESIAN_POINT ( 'NONE',  ( -229.7325401777437435, 4.600266235519089975, 11.08951027562286384 ) ) ;
#6534=ORIENTED_EDGE ( 'NONE', *, *, #12587, .T. ) ;
#6548=CARTESIAN_POINT ( 'NONE',  ( -242.1349625642079388, -6.437046975752621414, -10.12773524509340284 ) ) ;
#6550=CYLINDRICAL_SURFACE ( 'NONE', #7708, 230.0000000000000000 ) ;
#6590=CARTESIAN_POINT ( 'NONE',  ( -239.3907828020602153, 1.719565078627272259, 11.87615879295651311 ) ) ;
#6593=CARTESIAN_POINT ( 'NONE',  ( -245.8615520224613249, -9.158310437683550020, 7.754087231521529233 ) ) ;
#6615=CARTESIAN_POINT ( 'NONE',  ( -229.8662995960750379, -9.087301588047655088, 7.845977234077500917 ) ) ;
#6643=( NAMED_UNIT ( * ) PLANE_ANGLE_UNIT ( ) SI_UNIT ( $, .RADIAN. ) );
#6644=B_SPLINE_CURVE_WITH_KNOTS ( 'NONE', 3,
 ( #10268, #5581, #210, #12710, #12343, #4200, #9643, #11341, #11657, #11411, #2208, #6284, #277, #10334, #5270, #525, #9341, #4268, #2267, #6345, #1275, #8654, #8413, #5340, #3325, #2511, #4333, #12474, #7584, #6593, #3574, #7646, #1644, #2897, #4703, #784, #12588, #10844, #1716, #7983, #8849, #5985, #4774, #7777, #11040, #1914, #7841, #12910, #2763, #10910, #10044, #723, #2637, #12046, #2697, #1788, #3841, #9979, #8781, #3713, #11913, #5783, #6850, #10980, #9843, #6921, #3772, #4908, #5854, #6981, #5712, #9912, #3909, #4834, #9771, #6726, #850, #8917, #9046, #7909, #8047, #12846, #1852, #12978, #916, #11981, #11850, #2832, #652, #5916, #8981, #4974, #6419, #3971, #10778, #6787, #11175 ),
 .UNSPECIFIED., .F., .F.,
 ( 4, 1, 1, 2, 2, 2, 1, 1, 1, 2, 2, 2, 2, 1, 1, 1, 2, 2, 2, 1, 1, 1, 2, 2, 2, 1, 1, 1, 1, 2, 2, 2, 1, 1, 1, 2, 2, 1, 1, 1, 1, 2, 2, 2, 2, 1, 1, 1, 2, 2, 2, 2, 1, 1, 1, 2, 2, 2, 1, 1, 1, 2, 2, 4 ),
 ( 0.000000000000000000, 0.03125000000007535639, 0.04687500000011302070, 0.05468750000013182511, 0.06250000000015062951, 0.09375000000022588875, 0.1093750000002635253, 0.1171875000002850359, 0.1210937500002958050, 0.1230468750003012174, 0.1250000000003066158, 0.1875000000002915723, 0.2187500000002840506, 0.2343750000002802203, 0.2421875000002760014, 0.2460937500002739475, 0.2480468750002728928, 0.2500000000002718381, 0.2812500000002386980, 0.2968750000002220446, 0.3046875000002159939, 0.3085937500002151057, 0.3105468750002147726, 0.3125000000002144396, 0.3437500000002070566, 0.3593750000002033929, 0.3671875000002014500, 0.3710937500002023937, 0.3730468750002007838, 0.3740234375002000067, 0.3750000000001991740, 0.4062500000001449396, 0.4218750000001178502, 0.4296875000001044165, 0.4335937500000993650, 0.4355468750000968114, 0.4375000000000942579, 0.4687500000000812683, 0.4843750000000728306, 0.4921875000000685563, 0.4960937500000662248, 0.4980468750000652256, 0.5000000000000641709, 0.5625000000000439648, 0.5937500000000357492, 0.6093750000000297540, 0.6171875000000246470, 0.6210937500000223155, 0.6230468750000212053, 0.6250000000000199840, 0.6875000000000007772, 0.7187499999999896749, 0.7343749999999842348, 0.7421874999999797939, 0.7460937499999792388, 0.7480468749999805711, 0.7499999999999817923, 0.8125000000000066613, 0.8437500000000190958, 0.8593750000000254241, 0.8671875000000272005, 0.8710937500000280886, 0.8750000000000289768, 1.000000000000000000 ),
 .UNSPECIFIED. ) ;
#6663=CARTESIAN_POINT ( 'NONE',  ( -229.8660307814922987, 9.077839160772928295, 7.850369537300845302 ) ) ;
#6685=CARTESIAN_POINT ( 'NONE',  ( -240.2229988806957124, -3.132498172368823219, -11.58475653430379637 ) ) ;
#6686=DIRECTION ( 'NONE',  ( 1.000000000000000000, 0.000000000000000000, 0.000000000000000000 ) ) ;
#6688=ORIENTED_EDGE ( 'NONE', *, *, #3579, .T. ) ;
#6711=CARTESIAN_POINT ( 'NONE',  ( 0.000000000000000000, 0.000000000000000000, 0.000000000000000000 ) ) ;
#6715=CARTESIAN_POINT ( 'NONE',  ( -249.7118339206215012, -9.997999799959989886, -6.636264009214830395 ) ) ;
#6726=CARTESIAN_POINT ( 'NONE',  ( -241.9339721712941866, -6.203520525772937333, 10.27503750702521224 ) ) ;
#6728=CARTESIAN_POINT ( 'NONE',  ( -238.6985546758615442, -1.431921744593627863E-13, 12.00000000011287504 ) ) ;
#6731=CARTESIAN_POINT ( 'NONE',  ( -229.8321229872749143, 8.181811570953646751, 8.792102906095127679 ) ) ;
#6783=CARTESIAN_POINT ( 'NONE',  ( -249.7118339206215012, -9.997999799959989886, 6.636264009214830395 ) ) ;
#6787=CARTESIAN_POINT ( 'NONE',  ( -240.0746691521297578, -2.719637366637591036, 11.70176364698651561 ) ) ;
#6788=CARTESIAN_POINT ( 'NONE',  ( -238.7054772606637414, 0.2144843524526476863, -11.99854086871946635 ) ) ;
#6800=DIRECTION ( 'NONE',  ( 1.000000000000000000, 0.000000000000000000, 0.000000000000000000 ) ) ;
#6803=CARTESIAN_POINT ( 'NONE',  ( -240.2963067560768025, 3.341048620542326208, 11.52705098701326847 ) ) ;
#6810=CARTESIAN_POINT ( 'NONE',  ( -242.2936178119639123, -6.614827065997419098, -10.01219624237291761 ) ) ;
#6812=LINE ( 'NONE', #12066, #5805 ) ;
#6846=CARTESIAN_POINT ( 'NONE',  ( -249.7380656782638368, -10.65316887766604381, 5.649205583156061472 ) ) ;
#6847=DIRECTION ( 'NONE',  ( 1.000000000000000000, 0.000000000000000000, 0.000000000000000000 ) ) ;
#6850=CARTESIAN_POINT ( 'NONE',  ( -243.4994605518340620, -7.743136872103179691, 9.167522614742150466 ) ) ;
#6852=CARTESIAN_POINT ( 'NONE',  ( -239.0755113754114802, 1.313873757884649329, -11.92786187209476623 ) ) ;
#6862=EDGE_LOOP ( 'NONE', ( #2308, #2106, #11565, #8569, #3175, #11445, #6534, #7830, #2614, #2458, #10225, #12209 ) ) ;
#6867=CARTESIAN_POINT ( 'NONE',  ( -240.3908911752174333, 3.583360156783556683, 11.45287536843322052 ) ) ;
#6875=CARTESIAN_POINT ( 'NONE',  ( -229.9813818884356067, -11.63826747946651530, -2.948217368118681403 ) ) ;
#6877=ORIENTED_EDGE ( 'NONE', *, *, #6227, .F. ) ;
#6892=ORIENTED_EDGE ( 'NONE', *, *, #12723, .F. ) ;
#6918=CARTESIAN_POINT ( 'NONE',  ( -249.7604317440028296, -11.15122115098357014, 4.588451767773564782 ) ) ;
#6921=CARTESIAN_POINT ( 'NONE',  ( -242.7490684265873711, -7.085544781346608367, 9.685620095554028808 ) ) ;
#6931=CARTESIAN_POINT ( 'NONE',  ( -249.7118339206215012, 9.997999799959989886, -6.636264009214830395 ) ) ;
#6938=EDGE_CURVE ( 'NONE', #9902, #644, #1811, .T. ) ;
#6955=CARTESIAN_POINT ( 'NONE',  ( -239.0946434582524489, -1.343932714108268645, 11.92448114257838121 ) ) ;
#6965=CARTESIAN_POINT ( 'NONE',  ( -239.4471451945621254, -1.776586343123336853, -11.86775802751313869 ) ) ;
#6981=CARTESIAN_POINT ( 'NONE',  ( -242.3889174895368228, -6.718220498460057755, 9.943174756676034676 ) ) ;
#6992=CARTESIAN_POINT ( 'NONE',  ( -247.6787047776036559, 9.753293420611971243, -6.991498264524891759 ) ) ;
#6995=CARTESIAN_POINT ( 'NONE',  ( -243.4327047837443274, 7.689587473932653516, 9.212521827026886712 ) ) ;
#7013=DIRECTION ( 'NONE',  ( 0.000000000000000000, 0.000000000000000000, 1.000000000000000000 ) ) ;
#7021=CARTESIAN_POINT ( 'NONE',  ( -238.8648708971568624, -0.8933728624606902535, 11.96676141197713505 ) ) ;
#7031=CARTESIAN_POINT ( 'NONE',  ( -238.7551951684716869, -0.5376686924967483128, -11.98842779547521609 ) ) ;
#7050=CARTESIAN_POINT ( 'NONE',  ( -239.3393815581031561, 1.669038143830544607, -11.88372659505663798 ) ) ;
#7055=CARTESIAN_POINT ( 'NONE',  ( -246.2633612345466645, -9.321506464518613200, -7.557087660178679833 ) ) ;
#7065=CARTESIAN_POINT ( 'NONE',  ( -247.2298618829602503, 9.638957510244241078, 7.147826786188287151 ) ) ;
#7066=EDGE_CURVE ( 'NONE', #11098, #12785, #3776, .T. ) ;
#7096=CARTESIAN_POINT ( 'NONE',  ( -239.1634599900678495, -1.446074388866761540, -11.91252809098397236 ) ) ;
#7131=CARTESIAN_POINT ( 'NONE',  ( -247.9991062033159039, 9.816924796666317121, -6.901310522998599595 ) ) ;
#7134=CARTESIAN_POINT ( 'NONE',  ( -249.7118339206215012, 9.997999799959989886, 6.636264009214830395 ) ) ;
#7183=CARTESIAN_POINT ( 'NONE',  ( -246.0119047622995936, -9.221725594001977555, -7.678802609089674824 ) ) ;
#7186=EDGE_CURVE ( 'NONE', #1872, #7466, #5397, .T. ) ;
#7188=CARTESIAN_POINT ( 'NONE',  ( -245.5719560649888251, 9.027896078028849303, -7.905358857574679377 ) ) ;
#7208=CARTESIAN_POINT ( 'NONE',  ( -233.0000000000000000, 0.000000000000000000, 0.000000000000000000 ) ) ;
#7251=ORIENTED_EDGE ( 'NONE', *, *, #7186, .F. ) ;
#7253=CARTESIAN_POINT ( 'NONE',  ( -243.4327047836247573, -7.689587473836074771, -9.212521827111036288 ) ) ;
#7258=CARTESIAN_POINT ( 'NONE',  ( -242.3388033300362281, 6.664155345735165881, -9.979432606292707675 ) ) ;
#7265=ADVANCED_FACE ( 'NONE', ( #10306 ), #11518, .T. ) ;
#7269=ORIENTED_EDGE ( 'NONE', *, *, #4487, .T. ) ;
#7277=CARTESIAN_POINT ( 'NONE',  ( -250.0000000000000000, 0.000000000000000000, 0.000000000000000000 ) ) ;
#7307=DIRECTION ( 'NONE',  ( 0.000000000000000000, -1.000000000000000000, 0.000000000000000000 ) ) ;
#7320=CARTESIAN_POINT ( 'NONE',  ( -246.1949466613016284, -9.295128601147414571, -7.589564690491403809 ) ) ;
#7325=CARTESIAN_POINT ( 'NONE',  ( -240.5462192425209764, 3.949737371798292873, -11.33143176614105307 ) ) ;
#7326=CARTESIAN_POINT ( 'NONE',  ( -239.0198605536209868, 1.219845044661834521, 11.93783858050256796 ) ) ;
#7330=CARTESIAN_POINT ( 'NONE',  ( -229.7138320264111258, 3.546086608952734753, -11.47018943898591559 ) ) ;
#7359=AXIS2_PLACEMENT_3D ( 'NONE', #5455, #4573, #653 ) ;
#7377=CARTESIAN_POINT ( 'NONE',  ( -247.0556047488532840, 9.588534006617832617, 7.215007616888431841 ) ) ;
#7388=CARTESIAN_POINT ( 'NONE',  ( -242.5248711414777461, 6.860954770765020250, -9.845341009612386785 ) ) ;
#7389=CARTESIAN_POINT ( 'NONE',  ( -239.8750565987691061, 2.115697798598445978, 11.81209311377322813 ) ) ;
#7393=CARTESIAN_POINT ( 'NONE',  ( -229.8079896091062153, 7.470059805363084671, -9.398818199247862992 ) ) ;
#7440=CARTESIAN_POINT ( 'NONE',  ( -244.7822625628474213, 8.616351828725139939, 8.352152985389436068 ) ) ;
#7453=CARTESIAN_POINT ( 'NONE',  ( -242.4607547118677076, 6.794574172261055089, -9.891349720023484338 ) ) ;
#7454=CARTESIAN_POINT ( 'NONE',  ( -239.0779495979048477, 1.320275893629169639, 11.92738862982784021 ) ) ;
#7466=VERTEX_POINT ( 'NONE', #6715 ) ;
#7482=CARTESIAN_POINT ( 'NONE',  ( -229.8469569043687670, -8.584093440156065569, 8.393536236380878535 ) ) ;
#7519=CARTESIAN_POINT ( 'NONE',  ( -242.6565958084028125, 6.994822115566234899, -9.751204002521671299 ) ) ;
#7520=CARTESIAN_POINT ( 'NONE',  ( -238.7769902278642462, 0.6179568203354762757, 11.98408500534410948 ) ) ;
#7527=CARTESIAN_POINT ( 'NONE',  ( -229.8466722354996534, 8.576484730279149815, 8.401311290977700352 ) ) ;
#7542=B_SPLINE_CURVE_WITH_KNOTS ( 'NONE', 3,
 ( #5520, #7984, #12373, #5785, #12979, #4975, #5986, #5035, #12048, #8851, #5918, #3972, #885, #6054, #9845, #12178, #4041, #8049, #1980, #11043, #7050, #2833, #918, #3842, #5855, #6852, #10108, #7842, #4838, #8117, #9914, #4775, #9982, #981, #9047, #851, #10845, #9110, #7911, #10912, #2898, #6788, #1717, #11111 ),
 .UNSPECIFIED., .F., .F.,
 ( 4, 2, 2, 2, 2, 2, 2, 1, 1, 1, 2, 2, 2, 2, 1, 1, 2, 2, 2, 2, 1, 2, 2, 2, 4 ),
 ( 0.000000000000000000, 0.06252861007222769441, 0.07034468633125084969, 0.07425272446076752741, 0.07816076259028420514, 0.09379291510834281143, 0.1094250676264014316, 0.1172411438854389504, 0.1211491820149575849, 0.1231032010797020321, 0.1240802106120912213, 0.1250572201444804243, 0.1875858302175758274, 0.2188501352541234735, 0.2344822877723924670, 0.2422983640315269638, 0.2462064021610991527, 0.2501144402906713138, 0.3126430503639207048, 0.3439073554005454558, 0.3595395079188577481, 0.3673555841780140052, 0.3751716604371702068, 0.4377002705104277580, 0.5002288805836853092 ),
 .UNSPECIFIED. ) ;
#7544=CARTESIAN_POINT ( 'NONE',  ( -241.9271341488148153, -6.190796897788312769, -10.28045873088825957 ) ) ;
#7546=CARTESIAN_POINT ( 'NONE',  ( -229.7189907529219681, -3.915537799265266017, 11.36770974954495195 ) ) ;
#7560=CARTESIAN_POINT ( 'NONE',  ( -233.0000000000000000, 1.000000000000000000, -11.95826074310140008 ) ) ;
#7582=CARTESIAN_POINT ( 'NONE',  ( -238.7702306800076428, 0.5911393334065133676, 11.98543574551528401 ) ) ;
#7584=CARTESIAN_POINT ( 'NONE',  ( -246.0505219340116980, -9.238338704761243747, 7.658960895840565719 ) ) ;
#7587=CARTESIAN_POINT ( 'NONE',  ( -229.9997784648330708, 11.99578910728947712, -0.3697823523935888090 ) ) ;
#7606=CARTESIAN_POINT ( 'NONE',  ( -229.8371538172024771, -8.318415249073295215, 8.657075633561293060 ) ) ;
#7628=CARTESIAN_POINT ( 'NONE',  ( -229.6889200636375108, -1.000000000000000000, 11.95826074310140008 ) ) ;
#7641=FACE_OUTER_BOUND ( 'NONE', #9049, .T. ) ;
#7646=CARTESIAN_POINT ( 'NONE',  ( -245.6532195756332442, -9.065612403241397388, 7.862145249027526539 ) ) ;
#7649=CARTESIAN_POINT ( 'NONE',  ( -229.7396222156540944, 4.940198752275430927, 10.94224479212417300 ) ) ;
#7668=CARTESIAN_POINT ( 'NONE',  ( -240.0092717900809873, -2.435426586977146535, -11.75368411293068682 ) ) ;
#7669=CARTESIAN_POINT ( 'NONE',  ( -229.8082689465775559, -7.478642794604872357, 9.391993320510708898 ) ) ;
#7707=CARTESIAN_POINT ( 'NONE',  ( -249.7601711286370971, -11.14534860557855822, -4.601188512101209938 ) ) ;
#7708=AXIS2_PLACEMENT_3D ( 'NONE', #414, #2597, #6686 ) ;
#7715=CARTESIAN_POINT ( 'NONE',  ( -230.0000037765768184, 12.00007008448874579, -0.1815857884241967868 ) ) ;
#7725=( GEOMETRIC_REPRESENTATION_CONTEXT ( 3 ) GLOBAL_UNCERTAINTY_ASSIGNED_CONTEXT ( ( #12114 ) ) GLOBAL_UNIT_ASSIGNED_CONTEXT ( ( #4426, #6516, #4492 ) ) REPRESENTATION_CONTEXT ( 'NONE', 'WORKASPACE' ) );
#7727=CARTESIAN_POINT ( 'NONE',  ( -240.4848270099804779, 3.809198625029032836, 11.37937944661116596 ) ) ;
#7737=CARTESIAN_POINT ( 'NONE',  ( -229.8466860526774838, -8.576889844641714333, -8.400978990607617547 ) ) ;
#7751=DIRECTION ( 'NONE',  ( 0.000000000000000000, 0.000000000000000000, 1.000000000000000000 ) ) ;
#7777=CARTESIAN_POINT ( 'NONE',  ( -244.8348239361274352, -8.646460184833234308, 8.320981818661996599 ) ) ;
#7778=CIRCLE ( 'NONE', #3092, 12.00000000000000000 ) ;
#7784=CARTESIAN_POINT ( 'NONE',  ( -229.9928007510749524, 11.86142183433858577, -1.856684144637750666 ) ) ;
#7793=CARTESIAN_POINT ( 'NONE',  ( -241.0259582382434473, 4.889855348911388511, 10.95996151967449705 ) ) ;
#7799=CARTESIAN_POINT ( 'NONE',  ( -242.2196200855140091, -6.532801875576883965, -10.06598912834544635 ) ) ;
#7800=CARTESIAN_POINT ( 'NONE',  ( -229.7113347995026231, -3.365903791379974752, -11.51977029171405853 ) ) ;
#7801=VERTEX_POINT ( 'NONE', #7560 ) ;
#7811=CARTESIAN_POINT ( 'NONE',  ( -239.6569666445801374, -1.960938217768839920, 11.83870082047461914 ) ) ;
#7817=DIRECTION ( 'NONE',  ( 0.000000000000000000, -1.000000000000000000, 0.000000000000000000 ) ) ;
#7830=ORIENTED_EDGE ( 'NONE', *, *, #2467, .T. ) ;
#7841=CARTESIAN_POINT ( 'NONE',  ( -244.7207088053502275, -8.581273367803877505, 8.388577729903433422 ) ) ;
#7842=CARTESIAN_POINT ( 'NONE',  ( -239.0463147780496058, 1.265540212841881118, -11.93307915084255555 ) ) ;
#7861=CARTESIAN_POINT ( 'NONE',  ( -242.0646888581063081, 6.354939415246917633, 10.17926273054569641 ) ) ;
#7866=CARTESIAN_POINT ( 'NONE',  ( -249.7118339206215012, -9.997999799959989886, -6.636264009214830395 ) ) ;
#7867=CARTESIAN_POINT ( 'NONE',  ( -229.9297054377521761, -10.57472760585867100, -5.721117632547625398 ) ) ;
#7871=DIRECTION ( 'NONE',  ( 1.000000000000000000, 0.000000000000000000, 0.000000000000000000 ) ) ;
#7882=CARTESIAN_POINT ( 'NONE',  ( -233.0000000000000000, -1.000000000000000000, -12.50000000000000000 ) ) ;
#7909=CARTESIAN_POINT ( 'NONE',  ( -241.4289589284794033, -5.524154699785203348, 10.65313710557979299 ) ) ;
#7911=CARTESIAN_POINT ( 'NONE',  ( -238.7879693988574559, 0.6590516398346927263, -11.98189593644098849 ) ) ;
#7919=CARTESIAN_POINT ( 'NONE',  ( -233.0000000000000000, 0.000000000000000000, -12.00000000000000000 ) ) ;
#7922=CARTESIAN_POINT ( 'NONE',  ( -248.8841473305337217, 9.947364712431371103, -6.711964937433803513 ) ) ;
#7937=DIRECTION ( 'NONE',  ( 1.000000000000000000, 0.000000000000000000, 0.000000000000000000 ) ) ;
#7951=EDGE_CURVE ( 'NONE', #9902, #644, #12853, .T. ) ;
#7956=CARTESIAN_POINT ( 'NONE',  ( -239.4529136422323461, -1.782225441812128164, 11.86690534211290959 ) ) ;
#7966=CARTESIAN_POINT ( 'NONE',  ( -239.7865846179036282, -2.059993154243251023, -11.82215868861702468 ) ) ;
#7983=CARTESIAN_POINT ( 'NONE',  ( -245.0420335985837426, -8.761757998096216582, 8.199751241974521321 ) ) ;
#7984=CARTESIAN_POINT ( 'NONE',  ( -239.8728792811782284, 2.114429109107689442, -11.81232488172176964 ) ) ;
#7996=CARTESIAN_POINT ( 'NONE',  ( -248.1924789796937887, 9.852676062574365901, -6.850256174774278506 ) ) ;
#8000=CARTESIAN_POINT ( 'NONE',  ( -245.8375576811710346, 9.148519945048249724, 7.766315672653775870 ) ) ;
#8007=CARTESIAN_POINT ( 'NONE',  ( -229.7324912792606426, -4.597989431066022092, -11.09053087651768799 ) ) ;
#8010=CARTESIAN_POINT ( 'NONE',  ( -250.0000000000000000, 1.469576158976823947E-15, 12.00000000000000000 ) ) ;
#8014=PLANE ( 'NONE',  #12826 ) ;
#8030=CARTESIAN_POINT ( 'NONE',  ( -239.0539063777619617, -1.278329027785976457, -11.93171797770810727 ) ) ;
#8047=CARTESIAN_POINT ( 'NONE',  ( -241.3656950238382706, -5.430352949019471964, 10.70105707677801021 ) ) ;
#8049=CARTESIAN_POINT ( 'NONE',  ( -239.4330564014918252, 1.762617352138328153, -11.86984317867509908 ) ) ;
#8061=CARTESIAN_POINT ( 'NONE',  ( -249.1334134316369671, 9.986442412964869675, 6.653676027890797151 ) ) ;
#8074=LINE ( 'NONE', #8010, #2234 ) ;
#8090=CARTESIAN_POINT ( 'NONE',  ( -239.2621195213464205, -1.577673503500558017, 11.89604841280030278 ) ) ;
#8105=VERTEX_POINT ( 'NONE', #6051 ) ;
#8117=CARTESIAN_POINT ( 'NONE',  ( -239.0387908900173386, 1.252775422852272058, -11.93442892142129885 ) ) ;
#8126=CARTESIAN_POINT ( 'NONE',  ( -243.6963328790141361, -7.900314958675253685, -9.035065364327605764 ) ) ;
#8156=COLOUR_RGB ( '', 0.66274510, 0.83137255, 0.94901961) ;
#8168=CARTESIAN_POINT ( 'NONE',  ( -239.5718914795530452, -1.891487842075796788, -11.85001484766223712 ) ) ;
#8195=CARTESIAN_POINT ( 'NONE',  ( -244.7967862068877594, -8.624712650514746670, -8.343521798357105723 ) ) ;
#8201=CARTESIAN_POINT ( 'NONE',  ( -245.6532195753607084, 9.065612403116238838, -7.862145249173209116 ) ) ;
#8229=CARTESIAN_POINT ( 'NONE',  ( -249.7118339206215012, 9.997999799959989886, -6.636264009214830395 ) ) ;
#8236=CARTESIAN_POINT ( 'NONE',  ( -238.7978133391466429, -0.6936645309432929452, -11.97993715202083820 ) ) ;
#8246=DIRECTION ( 'NONE',  ( 1.000000000000000000, 0.000000000000000000, 0.000000000000000000 ) ) ;
#8264=CARTESIAN_POINT ( 'NONE',  ( -242.3537289185128429, 6.680330754393353665, -9.968624625890335267 ) ) ;
#8269=CARTESIAN_POINT ( 'NONE',  ( -229.9452934870987519, 10.90465451554996434, -5.064158863968243551 ) ) ;
#8288=AXIS2_PLACEMENT_3D ( 'NONE', #7882, #12081, #10884 ) ;
#8290=VERTEX_POINT ( 'NONE', #241 ) ;
#8324=CARTESIAN_POINT ( 'NONE',  ( -244.4094253577036113, -8.392574414408105810, -8.577616036601044769 ) ) ;
#8331=CARTESIAN_POINT ( 'NONE',  ( -241.4851975125052377, 5.604998872377223051, -10.61066964826765080 ) ) ;
#8349=DIRECTION ( 'NONE',  ( 0.000000000000000000, 0.000000000000000000, -1.000000000000000000 ) ) ;
#8378=MECHANICAL_DESIGN_GEOMETRIC_PRESENTATION_REPRESENTATION('',(#713),#7725);
#8384=CARTESIAN_POINT ( 'NONE',  ( -242.9129853713322973, 7.240649582117769434, 9.569633193565069362 ) ) ;
#8402=CARTESIAN_POINT ( 'NONE',  ( -229.6930204784227385, 1.737490451635691713, -11.87941726754192828 ) ) ;
#8405=ORIENTED_EDGE ( 'NONE', *, *, #7066, .F. ) ;
#8410=DIRECTION ( 'NONE',  ( 0.000000000000000000, -1.000000000000000000, 0.000000000000000000 ) ) ;
#8413=CARTESIAN_POINT ( 'NONE',  ( -246.4205552533093169, -9.380328321255895219, 7.484021895908157695 ) ) ;
#8440=EDGE_LOOP ( 'NONE', ( #10206, #255, #6892, #7269 ) ) ;
#8450=CARTESIAN_POINT ( 'NONE',  ( -247.8064210922640882, 9.777989738606054360, 6.956369377637167339 ) ) ;
#8463=CARTESIAN_POINT ( 'NONE',  ( -241.3346421314153076, 5.383590977540964495, -10.72461093951445399 ) ) ;
#8464=CARTESIAN_POINT ( 'NONE',  ( -239.0315606904630954, 1.240325117213125328, 11.93572853651427756 ) ) ;
#8482=FACE_OUTER_BOUND ( 'NONE', #11501, .T. ) ;
#8485=EDGE_LOOP ( 'NONE', ( #3472, #10899 ) ) ;
#8524=CARTESIAN_POINT ( 'NONE',  ( -241.3656950238681134, 5.430352949065432533, -10.70105707677310924 ) ) ;
#8529=PRODUCT_DEFINITION_SHAPE ( 'NONE', 'NONE',  #2767 ) ;
#8530=CARTESIAN_POINT ( 'NONE',  ( -229.7803353249896361, 6.565431021940706380, -10.05160335400266369 ) ) ;
#8548=CARTESIAN_POINT ( 'NONE',  ( -239.0407087255592842, -1.256038987220895020, 11.93408471358068113 ) ) ;
#8569=ORIENTED_EDGE ( 'NONE', *, *, #11735, .F. ) ;
#8585=DIRECTION ( 'NONE',  ( 0.000000000000000000, -1.000000000000000000, 0.000000000000000000 ) ) ;
#8588=EDGE_CURVE ( 'NONE', #12985, #6295, #12205, .T. ) ;
#8590=CARTESIAN_POINT ( 'NONE',  ( -238.9851262181995821, 1.156799816864296115, 11.94414832311762709 ) ) ;
#8591=AXIS2_PLACEMENT_3D ( 'NONE', #5066, #1879, #9209 ) ;
#8596=CARTESIAN_POINT ( 'NONE',  ( -229.9963607380661870, 11.93083377190782279, 1.487518229564186445 ) ) ;
#8652=CARTESIAN_POINT ( 'NONE',  ( -239.4758390117360989, 1.805333157548462131, 11.86347296100405124 ) ) ;
#8654=CARTESIAN_POINT ( 'NONE',  ( -246.5457465981856160, -9.425397935063502430, 7.427386666392754577 ) ) ;
#8656=CARTESIAN_POINT ( 'NONE',  ( -229.9035215981751890, 9.983406791829001037, 6.668687660899911052 ) ) ;
#8663=CARTESIAN_POINT ( 'NONE',  ( -241.2864786002318453, 5.310083909468028551, 10.76118394184098825 ) ) ;
#8670=CARTESIAN_POINT ( 'NONE',  ( -241.4352517270689589, -5.538320168158482382, -10.64816312893004202 ) ) ;
#8696=DIRECTION ( 'NONE',  ( 0.000000000000000000, 0.000000000000000000, 1.000000000000000000 ) ) ;
#8706=ORIENTED_EDGE ( 'NONE', *, *, #7951, .F. ) ;
#8714=AXIS2_PLACEMENT_3D ( 'NONE', #2236, #7307, #9305 ) ;
#8720=CARTESIAN_POINT ( 'NONE',  ( -229.9210428544502065, 10.37906049596799463, 6.034458640445298450 ) ) ;
#8740=CARTESIAN_POINT ( 'NONE',  ( -229.8178335282108264, -7.766306225721687717, 9.155633550835144518 ) ) ;
#8781=CARTESIAN_POINT ( 'NONE',  ( -243.5834864928896195, -7.809424032089201440, 9.110990436359818645 ) ) ;
#8805=CARTESIAN_POINT ( 'NONE',  ( -240.7195678457707402, -4.326096554271789074, -11.19626641913139409 ) ) ;
#8806=CARTESIAN_POINT ( 'NONE',  ( -229.8758178857063399, -9.335232842866593828, -7.576971754760646327 ) ) ;
#8823=CARTESIAN_POINT ( 'NONE',  ( -238.8090076327945894, -0.7315829084426003215, 11.97771329485296299 ) ) ;
#8844=DIRECTION ( 'NONE',  ( 0.000000000000000000, 0.000000000000000000, -1.000000000000000000 ) ) ;
#8845=FACE_OUTER_BOUND ( 'NONE', #8440, .T. ) ;
#8846=CARTESIAN_POINT ( 'NONE',  ( -249.7118339206215012, -9.997999799959989886, -6.636264009214830395 ) ) ;
#8849=CARTESIAN_POINT ( 'NONE',  ( -244.9313462850813039, -8.700834631469609448, 8.264179333479736655 ) ) ;
#8851=CARTESIAN_POINT ( 'NONE',  ( -239.5624944925539239, 1.883403902577551969, -11.85129291162959042 ) ) ;
#8854=CARTESIAN_POINT ( 'NONE',  ( -229.8083007641753568, 7.475044586470752428, 9.389288305976632998 ) ) ;
#8869=CARTESIAN_POINT ( 'NONE',  ( -247.8580199586201616, -9.788721918629967433, -6.941247868461743131 ) ) ;
#8870=CARTESIAN_POINT ( 'NONE',  ( -230.0000048734746940, -12.00009112689273749, 0.1798068418026676774 ) ) ;
#8893=APPLICATION_CONTEXT ( 'automotive_design' ) ;
#8911=CARTESIAN_POINT ( 'NONE',  ( -238.6985546646470198, 6.516754929249349828E-09, -12.00000000011316459 ) ) ;
#8917=CARTESIAN_POINT ( 'NONE',  ( -241.6004288479487343, -5.767183905185619963, 10.52387470033283812 ) ) ;
#8921=ORIENTED_EDGE ( 'NONE', *, *, #12278, .T. ) ;
#8923=ORIENTED_EDGE ( 'NONE', *, *, #2036, .T. ) ;
#8935=CARTESIAN_POINT ( 'NONE',  ( -239.9450917581424960, 2.156506209390990136, 11.80463811257499884 ) ) ;
#8956=CARTESIAN_POINT ( 'NONE',  ( -239.4323407727675885, -1.761903427608783046, 11.86994927914708242 ) ) ;
#8977=CARTESIAN_POINT ( 'NONE',  ( -249.7834747117780125, -11.65132285575867499, 2.887446915639924949 ) ) ;
#8981=CARTESIAN_POINT ( 'NONE',  ( -240.5462192425719365, -3.949737371913570438, 11.33143176610938418 ) ) ;
#8995=CARTESIAN_POINT ( 'NONE',  ( -248.9599100168424286, 9.954851740884455680, -6.700860962377057639 ) ) ;
#8999=CIRCLE ( 'NONE', #907, 239.0000000000000000 ) ;
#9000=CARTESIAN_POINT ( 'NONE',  ( -246.2769436248093200, 9.326692435635235867, 7.550684327875636370 ) ) ;
#9007=CARTESIAN_POINT ( 'NONE',  ( -229.9988845225136629, -11.97869403736654803, 0.7401432946465542617 ) ) ;
#9023=ADVANCED_FACE ( 'NONE', ( #9182 ), #2797, .T. ) ;
#9046=CARTESIAN_POINT ( 'NONE',  ( -241.4851975124299486, -5.604998872266711452, 10.61066964827916337 ) ) ;
#9047=CARTESIAN_POINT ( 'NONE',  ( -238.8209209945083273, 0.7687232794247820244, -11.97535954144907500 ) ) ;
#9049=EDGE_LOOP ( 'NONE', ( #4165, #5689, #9884, #1562, #3255, #6242, #10093, #12936, #6877, #5924, #11431, #1776 ) ) ;
#9061=DIRECTION ( 'NONE',  ( 0.000000000000000000, -1.000000000000000000, 0.000000000000000000 ) ) ;
#9064=CARTESIAN_POINT ( 'NONE',  ( -242.6194444007928439, 6.961689675959383372, 9.776526357768153375 ) ) ;
#9086=CARTESIAN_POINT ( 'NONE',  ( -239.5355863986199836, -1.859542203694944051, 11.85503690034565416 ) ) ;
#9094=CARTESIAN_POINT ( 'NONE',  ( -238.9264504976112846, -1.042958814602677364, -11.95497062546909639 ) ) ;
#9110=CARTESIAN_POINT ( 'NONE',  ( -238.7910754938288846, 0.6701662195168923697, -11.98127733922759042 ) ) ;
#9114=CARTESIAN_POINT ( 'NONE',  ( -247.8064210917818855, -9.777989738504603068, -6.956369377821547850 ) ) ;
#9120=CARTESIAN_POINT ( 'NONE',  ( -246.6520855319178906, 9.461709547860877478, -7.381047754363233793 ) ) ;
#9124=CARTESIAN_POINT ( 'NONE',  ( -244.7098307144296996, 8.574293600822041839, 8.395350236016119183 ) ) ;
#9151=ORIENTED_EDGE ( 'NONE', *, *, #1586, .T. ) ;
#9153=AXIS2_PLACEMENT_3D ( 'NONE', #256, #12582, #6523 ) ;
#9158=CARTESIAN_POINT ( 'NONE',  ( -239.4322611284946731, -1.761824011993069705, -11.86996097360714053 ) ) ;
#9181=TOROIDAL_SURFACE ( 'NONE', #884, 250.0000000000000000, 10.00000000000000000 ) ;
#9182=FACE_OUTER_BOUND ( 'NONE', #2440, .T. ) ;
#9186=CARTESIAN_POINT ( 'NONE',  ( -244.6090102803748607, -8.514624250321579879, -8.455955372765057376 ) ) ;
#9191=CARTESIAN_POINT ( 'NONE',  ( -249.3376476198023681, 9.985526825732678802, -6.655116011130676412 ) ) ;
#9209=DIRECTION ( 'NONE',  ( 1.000000000000000000, 0.000000000000000000, 0.000000000000000000 ) ) ;
#9228=CARTESIAN_POINT ( 'NONE',  ( -238.7907910596442207, -0.6691544179571565776, -11.98133399144852440 ) ) ;
#9254=CARTESIAN_POINT ( 'NONE',  ( -247.3711767290720616, -9.676486748149162764, -7.096931843143912566 ) ) ;
#9260=CARTESIAN_POINT ( 'NONE',  ( -240.5954930647663161, 4.058997395297933686, -11.29299565157840668 ) ) ;
#9297=ORIENTED_EDGE ( 'NONE', *, *, #7951, .T. ) ;
#9305=DIRECTION ( 'NONE',  ( 1.000000000000000000, 0.000000000000000000, 0.000000000000000000 ) ) ;
#9311=ORIENTED_EDGE ( 'NONE', *, *, #4481, .T. ) ;
#9322=CARTESIAN_POINT ( 'NONE',  ( -241.3090253319704743, 5.344653766046771004, -10.74405649903250470 ) ) ;
#9341=CARTESIAN_POINT ( 'NONE',  ( -247.6787047799290065, -9.753293421073170322, 6.991498263521549461 ) ) ;
#9377=CARTESIAN_POINT ( 'NONE',  ( -247.0695545831997890, 9.592608482329058717, 7.209588857402760453 ) ) ;
#9387=ORIENTED_EDGE ( 'NONE', *, *, #12510, .T. ) ;
#9391=CARTESIAN_POINT ( 'NONE',  ( -238.8104306093018181, 0.7422746157897220920, 11.97741946070771135 ) ) ;
#9408=DIRECTION ( 'NONE',  ( 0.000000000000000000, 1.000000000000000000, 0.000000000000000000 ) ) ;
#9422=EDGE_CURVE ( 'NONE', #12785, #8105, #6252, .T. ) ;
#9445=CARTESIAN_POINT ( 'NONE',  ( -242.2998418224646571, 6.621659878730367765, 10.00767884245070150 ) ) ;
#9453=DIRECTION ( 'NONE',  ( -1.000000000000000000, 0.000000000000000000, 0.000000000000000000 ) ) ;
#9457=CARTESIAN_POINT ( 'NONE',  ( -241.9339721714191853, 6.203520525929971718, -10.27503750700886087 ) ) ;
#9458=CARTESIAN_POINT ( 'NONE',  ( -238.7808081302305538, 0.6325455258416629034, 11.98332317327539798 ) ) ;
#9480=CARTESIAN_POINT ( 'NONE',  ( -229.9520201725233619, -11.04255732478361729, 4.700793194709331324 ) ) ;
#9496=ORIENTED_EDGE ( 'NONE', *, *, #6227, .T. ) ;
#9513=CARTESIAN_POINT ( 'NONE',  ( -240.0746691521900118, 2.719637366898895348, -11.70176364693860904 ) ) ;
#9514=CARTESIAN_POINT ( 'NONE',  ( -239.3224710781300644, 1.645298538954363066, 11.88664485503670853 ) ) ;
#9518=CARTESIAN_POINT ( 'NONE',  ( -229.9295651076812135, 10.57170285972954815, -5.726701700993176658 ) ) ;
#9562=SURFACE_SIDE_STYLE ('',( #1574 ) ) ;
#9582=VECTOR ( 'NONE', #9453, 1000.000000000000000 ) ;
#9636=CARTESIAN_POINT ( 'NONE',  ( -239.4202119743104902, 1.749723677800394839, 11.87175088374991994 ) ) ;
#9643=CARTESIAN_POINT ( 'NONE',  ( -248.8440518477580667, -9.943161799024673897, 6.718187330855736938 ) ) ;
#9647=CARTESIAN_POINT ( 'NONE',  ( -229.9519813856196606, 11.04228730818343251, 4.712348903618373441 ) ) ;
#9659=CARTESIAN_POINT ( 'NONE',  ( -240.4404613007375815, 3.704209566697797662, 11.41407139955384764 ) ) ;
#9665=CARTESIAN_POINT ( 'NONE',  ( -240.5991998574518220, -4.074980142339518885, -11.29000475009753579 ) ) ;
#9697=CARTESIAN_POINT ( 'NONE',  ( -250.0000000000000000, 0.000000000000000000, 0.000000000000000000 ) ) ;
#9698=CARTESIAN_POINT ( 'NONE',  ( -229.6889200636375108, -1.000000000000000000, -11.95826074310140008 ) ) ;
#9726=CARTESIAN_POINT ( 'NONE',  ( -229.6989920831166216, -2.478440081108693516, 11.76488731315652636 ) ) ;
#9737=CARTESIAN_POINT ( 'NONE',  ( -233.0000000000000000, 0.000000000000000000, 0.000000000000000000 ) ) ;
#9756=EDGE_LOOP ( 'NONE', ( #4326, #2632, #4869, #9496 ) ) ;
#9771=CARTESIAN_POINT ( 'NONE',  ( -242.1181102627692496, -6.423496681611010395, 10.13942498698713202 ) ) ;
#9775=CARTESIAN_POINT ( 'NONE',  ( -229.7675512415720789, 6.095529345594511206, 10.33836669620079185 ) ) ;
#9788=CARTESIAN_POINT ( 'NONE',  ( -240.4621951198816987, 3.755930367962047711, 11.39707303937045602 ) ) ;
#9796=CARTESIAN_POINT ( 'NONE',  ( -241.2266029203705102, -5.216955500352149500, -10.80672559041613212 ) ) ;
#9815=CARTESIAN_POINT ( 'NONE',  ( -238.7910754925967467, -0.6701662151381194699, 11.98127733947200646 ) ) ;
#9822=CARTESIAN_POINT ( 'NONE',  ( -229.9928407511759474, -11.86219540972909847, 1.851581510365113648 ) ) ;
#9843=CARTESIAN_POINT ( 'NONE',  ( -243.0412680530902207, -7.360923487768348927, 9.480357590559799874 ) ) ;
#9845=CARTESIAN_POINT ( 'NONE',  ( -239.4443750793461447, 1.773851997849018813, -11.86816533234759063 ) ) ;
#9864=DIRECTION ( 'NONE',  ( 0.000000000000000000, 0.000000000000000000, 1.000000000000000000 ) ) ;
#9884=ORIENTED_EDGE ( 'NONE', *, *, #10554, .T. ) ;
#9886=CARTESIAN_POINT ( 'NONE',  ( -239.7835669413218795, -2.057906908539555602, 11.82250766381889839 ) ) ;
#9900=ORIENTED_EDGE ( 'NONE', *, *, #4196, .T. ) ;
#9902=VERTEX_POINT ( 'NONE', #3293 ) ;
#9912=CARTESIAN_POINT ( 'NONE',  ( -242.3388033292662271, -6.664155344899789668, 9.979432606853753995 ) ) ;
#9914=CARTESIAN_POINT ( 'NONE',  ( -238.9765878232742580, 1.145734735638040735, -11.94560817730083890 ) ) ;
#9924=CARTESIAN_POINT ( 'NONE',  ( -245.4297298671266674, 8.960803861242091273, -7.981710862854209054 ) ) ;
#9931=CARTESIAN_POINT ( 'NONE',  ( -229.8080432352570313, -7.471644199020397004, -9.397490282286900865 ) ) ;
#9979=CARTESIAN_POINT ( 'NONE',  ( -243.6755871756507759, -7.880721788829696095, 9.049489450807712387 ) ) ;
#9982=CARTESIAN_POINT ( 'NONE',  ( -238.8648708987263376, 0.8933728665143385594, -11.96676141167906948 ) ) ;
#9986=ORIENTED_EDGE ( 'NONE', *, *, #2081, .T. ) ;
#9997=CARTESIAN_POINT ( 'NONE',  ( -243.9120028876667163, 8.059256684570714313, 8.893843983381984231 ) ) ;
#10018=CARTESIAN_POINT ( 'NONE',  ( -239.6279820725406751, -1.937806661696064969, 11.84250614284618131 ) ) ;
#10026=CARTESIAN_POINT ( 'NONE',  ( -239.4378968521887998, -1.767436680809186145, -11.86912576102403705 ) ) ;
#10038=ADVANCED_FACE ( 'NONE', ( #878 ), #8014, .F. ) ;
#10044=CARTESIAN_POINT ( 'NONE',  ( -244.2463344796078957, -8.285434989118469318, 8.680536403647563404 ) ) ;
#10056=ADVANCED_FACE ( 'NONE', ( #3196 ), #1143, .T. ) ;
#10062=CARTESIAN_POINT ( 'NONE',  ( -242.3038136696739002, 6.626013037278306150, 10.00479684789553048 ) ) ;
#10066=CARTESIAN_POINT ( 'NONE',  ( -229.7550362174501686, -5.611521452489740547, -10.61368970446696380 ) ) ;
#10091=CARTESIAN_POINT ( 'NONE',  ( -239.0379403834560605, -1.251320448579115618, -11.93458158033107175 ) ) ;
#10093=ORIENTED_EDGE ( 'NONE', *, *, #6394, .T. ) ;
#10098=ADVANCED_FACE ( 'NONE', ( #1518 ), #13036, .F. ) ;
#10108=CARTESIAN_POINT ( 'NONE',  ( -239.0548353904412124, 1.279873199972036968, -11.93155240843870146 ) ) ;
#10113=CARTESIAN_POINT ( 'NONE',  ( -247.0695545832770961, -9.592608482351387522, -7.209588857372366988 ) ) ;
#10118=CARTESIAN_POINT ( 'NONE',  ( -246.8633775079653390, 9.531357830558160771, -7.291317144092957392 ) ) ;
#10123=CARTESIAN_POINT ( 'NONE',  ( -249.8000249158748716, 12.00052859681964890, -0.5791969794655120740 ) ) ;
#10145=EDGE_CURVE ( 'NONE', #1872, #11418, #6644, .T. ) ;
#10149=CARTESIAN_POINT ( 'NONE',  ( -239.4316592316125707, -1.761224060149568116, -11.87005020869884220 ) ) ;
#10171=CARTESIAN_POINT ( 'NONE',  ( -247.8923716104523010, -9.795774998258135469, -6.931293060606263268 ) ) ;
#10178=CARTESIAN_POINT ( 'NONE',  ( -249.0734550457813725, 9.965425394255507996, -6.685150203396397650 ) ) ;
#10181=CARTESIAN_POINT ( 'NONE',  ( -245.0843090378622549, 8.789319854609475513, 8.173033110282421632 ) ) ;
#10206=ORIENTED_EDGE ( 'NONE', *, *, #6143, .T. ) ;
#10225=ORIENTED_EDGE ( 'NONE', *, *, #4481, .F. ) ;
#10243=CARTESIAN_POINT ( 'NONE',  ( -243.9120028947399987, -8.059256689375558835, -8.893843978839138131 ) ) ;
#10248=CARTESIAN_POINT ( 'NONE',  ( -242.3288872988346725, 6.653385920458625868, -9.986615906075055449 ) ) ;
#10268=CARTESIAN_POINT ( 'NONE',  ( -249.7118339206215012, -9.997999799959989886, 6.636264009214830395 ) ) ;
#10291=EDGE_CURVE ( 'NONE', #6137, #12985, #8999, .T. ) ;
#10306=FACE_OUTER_BOUND ( 'NONE', #11584, .T. ) ;
#10316=CARTESIAN_POINT ( 'NONE',  ( -242.3253012572110094, 6.649486011326967372, -9.989214338958454675 ) ) ;
#10330=AXIS2_PLACEMENT_3D ( 'NONE', #10574, #8585, #3632 ) ;
#10334=CARTESIAN_POINT ( 'NONE',  ( -247.9713910029833244, -9.811523844341806466, 6.908981293584625760 ) ) ;
#10374=CARTESIAN_POINT ( 'NONE',  ( -244.7098307116044111, -8.574293599168578695, -8.395350237759140910 ) ) ;
#10378=CARTESIAN_POINT ( 'NONE',  ( -241.6809225228018363, 5.875971056241065860, -10.46353150750831063 ) ) ;
#10379=CARTESIAN_POINT ( 'NONE',  ( -238.9657050040809452, 1.118917709522747828, 11.94772711066928750 ) ) ;
#10385=SHAPE_DEFINITION_REPRESENTATION ( #8529, #4340 ) ;
#10396=CARTESIAN_POINT ( 'NONE',  ( 0.000000000000000000, 1.000000000000000000, 0.000000000000000000 ) ) ;
#10422=MANIFOLD_SOLID_BREP ( 'NONE', #1780 ) ;
#10439=CARTESIAN_POINT ( 'NONE',  ( -244.8027971735120047, 8.628165349658024397, 8.339952776931941258 ) ) ;
#10450=ORIENTED_EDGE ( 'NONE', *, *, #8588, .T. ) ;
#10452=CARTESIAN_POINT ( 'NONE',  ( -243.5181255321104459, 7.757956330428964264, -9.154932349439130590 ) ) ;
#10453=CARTESIAN_POINT ( 'NONE',  ( -239.6598046819784145, 1.963348620848123893, 11.83831708201935839 ) ) ;
#10459=CARTESIAN_POINT ( 'NONE',  ( -229.7292463621831757, 4.422629786613017977, -11.15695835592746654 ) ) ;
#10465=CARTESIAN_POINT ( 'NONE',  ( -249.7894249019889230, 11.77854918022920039, -2.316202908582821074 ) ) ;
#10481=CARTESIAN_POINT ( 'NONE',  ( -229.9210444607178658, -10.37910877259903231, 6.034405755772844770 ) ) ;
#10517=AXIS2_PLACEMENT_3D ( 'NONE', #10396, #9408, #11410 ) ;
#10519=CARTESIAN_POINT ( 'NONE',  ( -243.8618317092203824, 8.020662184074344836, -8.926546575949515727 ) ) ;
#10520=CARTESIAN_POINT ( 'NONE',  ( -238.9057708211122133, 0.9926994598474889742, 11.95893060915291173 ) ) ;
#10525=CARTESIAN_POINT ( 'NONE',  ( -229.8466474081030526, 8.575819594941270552, -8.402010734614378862 ) ) ;
#10554=EDGE_CURVE ( 'NONE', #8105, #8290, #11782, .T. ) ;
#10574=CARTESIAN_POINT ( 'NONE',  ( 0.000000000000000000, -1.000000000000000000, 0.000000000000000000 ) ) ;
#10585=CARTESIAN_POINT ( 'NONE',  ( -229.9292789904498591, 10.55952007275214299, 5.712813050723659636 ) ) ;
#10601=CARTESIAN_POINT ( 'NONE',  ( -242.2998418224420050, -6.621659878705485447, -10.00767884246599415 ) ) ;
#10628=TOROIDAL_SURFACE ( 'NONE', #8714, 241.5000000000000000, 2.500000000000000000 ) ;
#10635=DIRECTION ( 'NONE',  ( 1.000000000000000000, 0.000000000000000000, 0.000000000000000000 ) ) ;
#10646=CARTESIAN_POINT ( 'NONE',  ( -239.2640814428857539, 1.577485845743592741, 11.89585958266493471 ) ) ;
#10691=VERTEX_POINT ( 'NONE', #12685 ) ;
#10713=AXIS2_PLACEMENT_3D ( 'NONE', #1568, #7817, #11892 ) ;
#10721=CARTESIAN_POINT ( 'NONE',  ( -229.9710684506134157, 11.43264861468415816, 3.665441760567183405 ) ) ;
#10731=CARTESIAN_POINT ( 'NONE',  ( -240.9204428197673451, 4.702057767962908308, 11.04114865026916270 ) ) ;
#10733=CARTESIAN_POINT ( 'NONE',  ( -233.0000000000000000, 0.000000000000000000, 0.000000000000000000 ) ) ;
#10738=CARTESIAN_POINT ( 'NONE',  ( -240.4848270099879528, -3.809198625046382070, -11.37937944660441048 ) ) ;
#10759=FACE_OUTER_BOUND ( 'NONE', #8485, .T. ) ;
#10765=DIRECTION ( 'NONE',  ( 0.000000000000000000, 0.000000000000000000, 1.000000000000000000 ) ) ;
#10766=DIRECTION ( 'NONE',  ( -1.000000000000000000, 0.000000000000000000, 0.000000000000000000 ) ) ;
#10778=CARTESIAN_POINT ( 'NONE',  ( -240.2579444296266615, -3.284593558526797352, 11.55663755358773415 ) ) ;
#10781=CARTESIAN_POINT ( 'NONE',  ( -229.7551259172103357, 5.607610899293940854, 10.61085097052528425 ) ) ;
#10814=CARTESIAN_POINT ( 'NONE',  ( -238.7981149109900514, -0.6946964185326648389, 11.97987716372956690 ) ) ;
#10841=CARTESIAN_POINT ( 'NONE',  ( -249.7894249019897188, -11.77854918023606601, 2.316202908502521307 ) ) ;
#10844=CARTESIAN_POINT ( 'NONE',  ( -245.3145835540676103, -8.904103460292617456, 8.045132556050477390 ) ) ;
#10845=CARTESIAN_POINT ( 'NONE',  ( -238.7981149122642250, 0.6946964228884829895, -11.97987716347747522 ) ) ;
#10847=CARTESIAN_POINT ( 'NONE',  ( -229.7140139254735800, 3.557752282343352945, 11.46654900609709848 ) ) ;
#10858=CARTESIAN_POINT ( 'NONE',  ( -241.4352517276585104, 5.538320169061370812, 10.64816312846143553 ) ) ;
#10868=CARTESIAN_POINT ( 'NONE',  ( -242.3038136696815457, -6.626013037286656804, -10.00479684789021917 ) ) ;
#10884=DIRECTION ( 'NONE',  ( 0.000000000000000000, 0.000000000000000000, 1.000000000000000000 ) ) ;
#10899=ORIENTED_EDGE ( 'NONE', *, *, #3204, .T. ) ;
#10910=CARTESIAN_POINT ( 'NONE',  ( -244.3545189506059216, -8.356296374751478240, 8.612604422907843116 ) ) ;
#10912=CARTESIAN_POINT ( 'NONE',  ( -238.7553599115560132, 0.5384408835009459882, -11.98839505287317841 ) ) ;
#10927=DIRECTION ( 'NONE',  ( 1.000000000000000000, 0.000000000000000000, 0.000000000000000000 ) ) ;
#10928=CARTESIAN_POINT ( 'NONE',  ( -242.2626230870823463, 6.580656946580349498, 10.03470782660452976 ) ) ;
#10933=AXIS2_PLACEMENT_3D ( 'NONE', #12311, #6186, #11446 ) ;
#10937=CARTESIAN_POINT ( 'NONE',  ( -229.8947343418161893, -9.784924124804621925, -6.986540743649005236 ) ) ;
#10956=CARTESIAN_POINT ( 'NONE',  ( -239.8728793007195179, -2.114429120494187408, 11.81232487964174638 ) ) ;
#10980=CARTESIAN_POINT ( 'NONE',  ( -243.2557941747326993, -7.548840531214802141, 9.332172165351044768 ) ) ;
#11014=CARTESIAN_POINT ( 'NONE',  ( -239.0755113761929920, -1.313873759170463673, 11.92786187197615000 ) ) ;
#11018=DIRECTION ( 'NONE',  ( -1.000000000000000000, 0.000000000000000000, 0.000000000000000000 ) ) ;
#11040=CARTESIAN_POINT ( 'NONE',  ( -244.8267157024196194, -8.641841620791439027, 8.325778331725320669 ) ) ;
#11043=CARTESIAN_POINT ( 'NONE',  ( -239.4329164351061365, 1.762478857497947971, -11.86986396130624044 ) ) ;
#11056=CARTESIAN_POINT ( 'NONE',  ( -246.4205552523959852, 9.380328320921323737, -7.484021896315862676 ) ) ;
#11060=CARTESIAN_POINT ( 'NONE',  ( -244.7967862073442120, 8.624712650776588774, 8.343521798077146556 ) ) ;
#11065=AXIS2_PLACEMENT_3D ( 'NONE', #9697, #1782, #8844 ) ;
#11085=CARTESIAN_POINT ( 'NONE',  ( -239.4443750393931509, -1.773851958419369712, 11.86816533821130015 ) ) ;
#11093=CARTESIAN_POINT ( 'NONE',  ( -238.8364110056832885, -0.8171106957274414384, -11.97229870871749746 ) ) ;
#11098=VERTEX_POINT ( 'NONE', #271 ) ;
#11102=CARTESIAN_POINT ( 'NONE',  ( -248.5207756042016172, 9.904443212642727090, -6.775263356373602441 ) ) ;
#11111=CARTESIAN_POINT ( 'NONE',  ( -238.6985546646470198, 6.516754929249349828E-09, -12.00000000011316459 ) ) ;
#11115=CARTESIAN_POINT ( 'NONE',  ( -245.0843090350436171, -8.789319852992315774, -8.173033111772259218 ) ) ;
#11125=CARTESIAN_POINT ( 'NONE',  ( -249.7999494874249251, 11.99892863384215325, 1.190337990169640703 ) ) ;
#11159=CARTESIAN_POINT ( 'NONE',  ( -239.2610567797048304, -1.576377190171931453, -11.89622111457706133 ) ) ;
#11175=CARTESIAN_POINT ( 'NONE',  ( -239.9450917581429792, -2.156506209390995021, 11.80463811257499884 ) ) ;
#11186=CARTESIAN_POINT ( 'NONE',  ( -246.3576883201962175, 9.357104192357786232, -7.512982112911617882 ) ) ;
#11191=CARTESIAN_POINT ( 'NONE',  ( -249.7969288063768545, 11.93744875557469953, -1.454679372240188506 ) ) ;
#11203=ADVANCED_FACE ( 'NONE', ( #12993 ), #3854, .F. ) ;
#11210=ORIENTED_EDGE ( 'NONE', *, *, #4437, .T. ) ;
#11243=CARTESIAN_POINT ( 'NONE',  ( -243.4813404522815290, -7.728679802368493945, -9.179736092244947798 ) ) ;
#11248=ORIENTED_EDGE ( 'NONE', *, *, #10145, .T. ) ;
#11254=CARTESIAN_POINT ( 'NONE',  ( -245.5556485997058758, 9.020247694294253549, -7.914083889464029298 ) ) ;
#11261=CARTESIAN_POINT ( 'NONE',  ( -229.9651094064373638, 11.31238621391031529, -4.021116903567067524 ) ) ;
#11292=CARTESIAN_POINT ( 'NONE',  ( -239.1339513535814945, -1.403748199837580035, -11.91760216378363424 ) ) ;
#11314=CARTESIAN_POINT ( 'NONE',  ( 0.000000000000000000, -9.997999799959989886, 0.000000000000000000 ) ) ;
#11319=CARTESIAN_POINT ( 'NONE',  ( -246.2429388857162280, -9.313684383457655258, -7.566737218363915218 ) ) ;
#11323=CARTESIAN_POINT ( 'NONE',  ( -245.0420335974988006, 8.761757997507153561, -8.199751242572485666 ) ) ;
#11341=CARTESIAN_POINT ( 'NONE',  ( -248.6652334677784779, -9.923450225169199612, 6.747319395809158848 ) ) ;
#11387=CARTESIAN_POINT ( 'NONE',  ( -247.0236966365115450, -9.579141830393634649, -7.227478268642161474 ) ) ;
#11394=CARTESIAN_POINT ( 'NONE',  ( -240.5255509705628469, 3.902938849068647631, -11.34756747382315112 ) ) ;
#11410=DIRECTION ( 'NONE',  ( 1.000000000000000000, 0.000000000000000000, 1.421085471520200056E-14 ) ) ;
#11411=CARTESIAN_POINT ( 'NONE',  ( -248.3022220597990781, -9.870789006701004453, 6.824104388389867104 ) ) ;
#11418=VERTEX_POINT ( 'NONE', #69 ) ;
#11431=ORIENTED_EDGE ( 'NONE', *, *, #3204, .F. ) ;
#11440=CARTESIAN_POINT ( 'NONE',  ( -247.6855308008555596, 9.751870871517551720, 6.992977237921749634 ) ) ;
#11445=ORIENTED_EDGE ( 'NONE', *, *, #8588, .F. ) ;
#11446=DIRECTION ( 'NONE',  ( 1.000000000000000000, 0.000000000000000000, 0.000000000000000000 ) ) ;
#11455=CARTESIAN_POINT ( 'NONE',  ( -244.0248830888228895, 8.135989420001589423, -8.821260460353125055 ) ) ;
#11484=CARTESIAN_POINT ( 'NONE',  ( -229.9035141788515375, -9.983227244538054990, 6.668950963032000523 ) ) ;
#11501=EDGE_LOOP ( 'NONE', ( #11886, #11210 ) ) ;
#11512=CARTESIAN_POINT ( 'NONE',  ( -249.7118339206215012, 9.997999799959989886, -6.636264009214830395 ) ) ;
#11513=FILL_AREA_STYLE_COLOUR ( '', #8156 ) ;
#11518=CYLINDRICAL_SURFACE ( 'NONE', #10933, 249.7999999999999829 ) ;
#11528=CARTESIAN_POINT ( 'NONE',  ( -240.9947549591053928, 4.840187564906756279, -10.98379185745642239 ) ) ;
#11565=ORIENTED_EDGE ( 'NONE', *, *, #10145, .F. ) ;
#11567=EDGE_LOOP ( 'NONE', ( #8921, #8923, #7251, #11248 ) ) ;
#11572=EDGE_CURVE ( 'NONE', #6137, #5558, #5187, .T. ) ;
#11584=EDGE_LOOP ( 'NONE', ( #123, #3332 ) ) ;
#11592=CARTESIAN_POINT ( 'NONE',  ( -244.1671264060107660, 8.232476465879829064, -8.730683390178871406 ) ) ;
#11593=CARTESIAN_POINT ( 'NONE',  ( -238.7604407559926187, 0.5508784862251008274, 11.98739478578908013 ) ) ;
#11643=CARTESIAN_POINT ( 'NONE',  ( -249.7834747117774157, 11.65132285575429982, -2.887446915690841109 ) ) ;
#11657=CARTESIAN_POINT ( 'NONE',  ( -248.5207756069831930, -9.904443213030258875, 6.775263355895822848 ) ) ;
#11662=CARTESIAN_POINT ( 'NONE',  ( -229.9968423840866478, 11.93955909105315705, -1.301722993638689596 ) ) ;
#11679=CARTESIAN_POINT ( 'NONE',  ( -239.9450917581429792, -2.156506209390995021, -11.80463811257499884 ) ) ;
#11719=CYLINDRICAL_SURFACE ( 'NONE', #11065, 12.00000000000000000 ) ;
#11721=CARTESIAN_POINT ( 'NONE',  ( -249.7915528516605548, -11.82778639353378125, -2.343958593077331898 ) ) ;
#11735=EDGE_CURVE ( 'NONE', #7466, #1872, #5497, .T. ) ;
#11736=LINE ( 'NONE', #5598, #12139 ) ;
#11744=CARTESIAN_POINT ( 'NONE',  ( -240.0865915474315102, -2.714760371352697987, -11.69235895547828363 ) ) ;
#11746=ORIENTED_EDGE ( 'NONE', *, *, #2467, .F. ) ;
#11774=CARTESIAN_POINT ( 'NONE',  ( -249.7380656782619042, 10.65316887761970222, -5.649205583226009963 ) ) ;
#11782=CIRCLE ( 'NONE', #6033, 12.00000000000000000 ) ;
#11795=CARTESIAN_POINT ( 'NONE',  ( -229.7511168103433477, 5.440903037008435916, 10.69724303830294865 ) ) ;
#11806=CARTESIAN_POINT ( 'NONE',  ( 0.000000000000000000, -13.19999999999999929, 0.000000000000000000 ) ) ;
#11815=CARTESIAN_POINT ( 'NONE',  ( -241.8394219704672423, -6.081466909965556944, -10.34544425870726592 ) ) ;
#11816=CARTESIAN_POINT ( 'NONE',  ( -229.9812292664173015, -11.63484992564693599, 2.943925132602736028 ) ) ;
#11850=CARTESIAN_POINT ( 'NONE',  ( -240.9947549593328802, -4.840187565308244011, 10.98379185734033925 ) ) ;
#11854=CARTESIAN_POINT ( 'NONE',  ( -229.8036261751163352, 7.330002591760357511, 9.502943147174924832 ) ) ;
#11863=CARTESIAN_POINT ( 'NONE',  ( -241.2266029204368465, 5.216955500457195249, 10.80672559037492952 ) ) ;
#11871=CARTESIAN_POINT ( 'NONE',  ( -242.2626230869292101, -6.580656946410289088, -10.03470782670428996 ) ) ;
#11874=CARTESIAN_POINT ( 'NONE',  ( -229.6989039822362599, -2.469951368212909060, -11.76658813962577277 ) ) ;
#11884=CARTESIAN_POINT ( 'NONE',  ( -238.7879693975320947, -0.6590516350396603551, 11.98189593670389463 ) ) ;
#11886=ORIENTED_EDGE ( 'NONE', *, *, #3579, .F. ) ;
#11892=DIRECTION ( 'NONE',  ( 1.000000000000000000, 0.000000000000000000, 0.000000000000000000 ) ) ;
#11911=CARTESIAN_POINT ( 'NONE',  ( 0.000000000000000000, 0.000000000000000000, 0.000000000000000000 ) ) ;
#11913=CARTESIAN_POINT ( 'NONE',  ( -243.5181255321092522, -7.757956330428957159, 9.154932349471659236 ) ) ;
#11929=CARTESIAN_POINT ( 'NONE',  ( -242.2196200858086286, 6.532801875907670919, 10.06598912815299229 ) ) ;
#11938=CARTESIAN_POINT ( 'NONE',  ( -244.7822625619571681, -8.616351828212369668, -8.352152985936292851 ) ) ;
#11940=CARTESIAN_POINT ( 'NONE',  ( -229.9990782680060306, -11.98248316673616110, -0.7483019246402946578 ) ) ;
#11955=CARTESIAN_POINT ( 'NONE',  ( -239.6024283181542955, -1.916856350840707268, 11.84591042646273173 ) ) ;
#11971=ORIENTED_EDGE ( 'NONE', *, *, #10554, .F. ) ;
#11981=CARTESIAN_POINT ( 'NONE',  ( -241.1422742072429628, -5.089614320943621095, 10.87069852631545963 ) ) ;
#12025=CARTESIAN_POINT ( 'NONE',  ( -239.4341775679679643, -1.763735199333067882, 11.86967692310885347 ) ) ;
#12046=CARTESIAN_POINT ( 'NONE',  ( -244.1511139035978317, -8.221670795503211338, 8.740858670380884377 ) ) ;
#12048=CARTESIAN_POINT ( 'NONE',  ( -239.6024283463667075, 1.916856374241466821, -11.84591042273142669 ) ) ;
#12056=CARTESIAN_POINT ( 'NONE',  ( -248.0636855450023575, 9.829232303934618997, -6.883789224338879187 ) ) ;
#12059=CARTESIAN_POINT ( 'NONE',  ( -244.2419534947191551, 8.283406883053094916, 8.682674417521349497 ) ) ;
#12066=CARTESIAN_POINT ( 'NONE',  ( -250.0000000000000000, -1.000000000000000000, 11.95826074310140008 ) ) ;
#12081=DIRECTION ( 'NONE',  ( 0.000000000000000000, 1.000000000000000000, 0.000000000000000000 ) ) ;
#12114=UNCERTAINTY_MEASURE_WITH_UNIT (LENGTH_MEASURE( 1.000000000000000082E-05 ), #4426, 'distance_accuracy_value', 'NONE');
#12119=VERTEX_POINT ( 'NONE', #7628 ) ;
#12128=CARTESIAN_POINT ( 'NONE',  ( -249.7601711286373529, 11.14534860556848983, 4.601188512082746485 ) ) ;
#12139=VECTOR ( 'NONE', #4587, 1000.000000000000000 ) ;
#12152=CARTESIAN_POINT ( 'NONE',  ( -238.8461604298144607, -0.8432863431609350924, 11.97040126094618273 ) ) ;
#12160=CARTESIAN_POINT ( 'NONE',  ( -239.0936989914653452, -1.342465038504252250, -11.92464663098946787 ) ) ;
#12178=CARTESIAN_POINT ( 'NONE',  ( -239.4371284606225743, 1.766671758494314570, -11.86923926621154912 ) ) ;
#12186=CARTESIAN_POINT ( 'NONE',  ( -247.0556047486957141, -9.588534006571833856, -7.215007616948605040 ) ) ;
#12192=CARTESIAN_POINT ( 'NONE',  ( -246.3021867260495412, 9.336273485133032679, -7.538834026437402080 ) ) ;
#12197=CARTESIAN_POINT ( 'NONE',  ( -249.7379166007384299, 10.64944549068976443, 5.654815128254504053 ) ) ;
#12205=B_SPLINE_CURVE_WITH_KNOTS ( 'NONE', 3,
 ( #3958, #2883, #13026, #4154, #7031, #5970, #9228, #8236, #6036, #11093, #5021, #9094, #12291, #10091, #832, #3144, #8030, #4021, #12160, #11292, #7096, #11159, #6098, #10149, #1024, #9158, #2156, #10026, #6965, #5083, #4088, #6233, #3892, #8168, #2086, #12229, #7966, #4892, #3083 ),
 .UNSPECIFIED., .F., .F.,
 ( 4, 2, 2, 2, 1, 1, 2, 2, 2, 1, 1, 2, 2, 2, 2, 1, 1, 1, 2, 2, 2, 2, 4 ),
 ( 0.5002288805836853092, 0.5627002705110166758, 0.6251716604383480425, 0.6329805841792639498, 0.6407895079201798572, 0.6564073554020164458, 0.6876430503656948412, 0.7501144402930455257, 0.7540189021635022026, 0.7579233640339586575, 0.7657322877748720114, 0.7813501352567079339, 0.8125858302203701200, 0.8750572201477042622, 0.8760333356153189310, 0.8770094510829338219, 0.8789616820181391788, 0.8828661438885272439, 0.8906750676292846114, 0.9062929151108138903, 0.9219107625923431693, 0.9375286100738724482, 1.000000000000000000 ),
 .UNSPECIFIED. ) ;
#12209=ORIENTED_EDGE ( 'NONE', *, *, #9422, .T. ) ;
#12229=CARTESIAN_POINT ( 'NONE',  ( -239.6598046804633384, -1.963348619657336425, -11.83831708221096690 ) ) ;
#12242=VECTOR ( 'NONE', #4912, 1000.000000000000000 ) ;
#12254=CIRCLE ( 'NONE', #10330, 230.0000000000000000 ) ;
#12256=CARTESIAN_POINT ( 'NONE',  ( -244.8027971735998847, -8.628165349708508458, -8.339952776884981489 ) ) ;
#12262=CARTESIAN_POINT ( 'NONE',  ( -247.9529057710629445, 9.807895050960942385, -6.914131050859374739 ) ) ;
#12278=EDGE_CURVE ( 'NONE', #11418, #6295, #5744, .T. ) ;
#12291=CARTESIAN_POINT ( 'NONE',  ( -238.9758744801582395, -1.144350540312424558, -11.94573993414358704 ) ) ;
#12304=LINE ( 'NONE', #6313, #1266 ) ;
#12311=CARTESIAN_POINT ( 'NONE',  ( 0.000000000000000000, -13.19999999999999929, 0.000000000000000000 ) ) ;
#12314=CARTESIAN_POINT ( 'NONE',  ( -245.7174131604188858, -9.095590352148393620, -7.828444976190365168 ) ) ;
#12325=CARTESIAN_POINT ( 'NONE',  ( -244.1419029264685605, 8.215433989563221573, -8.746719778180930049 ) ) ;
#12343=CARTESIAN_POINT ( 'NONE',  ( -248.9599100169513122, -9.954851740894934409, 6.700860962374001417 ) ) ;
#12373=CARTESIAN_POINT ( 'NONE',  ( -239.7835669211240202, 2.057906893573868246, -11.82250766619783278 ) ) ;
#12385=CARTESIAN_POINT ( 'NONE',  ( -242.9129853705333915, -7.240649581379505761, -9.569633194163635892 ) ) ;
#12389=CARTESIAN_POINT ( 'NONE',  ( -241.1422742070761558, 5.089614320685067916, -10.87069852639233147 ) ) ;
#12411=DIRECTION ( 'NONE',  ( 1.000000000000000000, 0.000000000000000000, 0.000000000000000000 ) ) ;
#12445=CARTESIAN_POINT ( 'NONE',  ( -245.7174131648644675, 9.095590354146871448, 7.828444973944560736 ) ) ;
#12452=CARTESIAN_POINT ( 'NONE',  ( -250.0000000000000000, -1.000000000000000000, -11.95826074310140008 ) ) ;
#12457=CARTESIAN_POINT ( 'NONE',  ( -243.5376947841724018, 7.773445842367202374, -9.141748602794347534 ) ) ;
#12458=CARTESIAN_POINT ( 'NONE',  ( -239.5448319005391511, 1.867756356064017131, 11.85375772827623742 ) ) ;
#12462=CARTESIAN_POINT ( 'NONE',  ( -229.7397366602772877, 4.937265191653261276, -10.93887086792326002 ) ) ;
#12472=DIRECTION ( 'NONE',  ( 1.000000000000000000, 0.000000000000000000, 0.000000000000000000 ) ) ;
#12474=CARTESIAN_POINT ( 'NONE',  ( -246.1739743505053184, -9.287690276134259904, 7.598953578806062481 ) ) ;
#12479=CARTESIAN_POINT ( 'NONE',  ( -238.6985546758615442, -1.431921744593627863E-13, 12.00000000011287504 ) ) ;
#12503=CARTESIAN_POINT ( 'NONE',  ( -242.2936178120088755, 6.614827066046929716, 10.01219624234327021 ) ) ;
#12504=FILL_AREA_STYLE ('',( #11513 ) ) ;
#12510=EDGE_CURVE ( 'NONE', #8290, #7801, #12789, .T. ) ;
#12517=CARTESIAN_POINT ( 'NONE',  ( -244.8348239360272771, 8.646460184776158187, -8.320981818718424350 ) ) ;
#12518=CARTESIAN_POINT ( 'NONE',  ( -239.1309277283428685, 1.402640123932128891, 11.91796374952781790 ) ) ;
#12531=CARTESIAN_POINT ( 'NONE',  ( -233.0000000000000000, 1.000000000000000000, -12.50000000000000000 ) ) ;
#12542=CARTESIAN_POINT ( 'NONE',  ( -229.9555022783201821, -11.11474285528676376, 4.527357793578296707 ) ) ;
#12554=CARTESIAN_POINT ( 'NONE',  ( -239.9450917581429792, -2.156506209390995021, -11.80463811257499884 ) ) ;
#12582=DIRECTION ( 'NONE',  ( -1.000000000000000000, 0.000000000000000000, 0.000000000000000000 ) ) ;
#12583=CARTESIAN_POINT ( 'NONE',  ( -242.1181102628582664, 6.423496681710723522, -10.13942498697665862 ) ) ;
#12587=EDGE_CURVE ( 'NONE', #12985, #4948, #11736, .T. ) ;
#12588=CARTESIAN_POINT ( 'NONE',  ( -245.4297298679771586, -8.960803861643656276, 7.981710862397758177 ) ) ;
#12590=CARTESIAN_POINT ( 'NONE',  ( -229.8945924270675221, 9.781573351764743407, -6.991165551757859475 ) ) ;
#12599=DIRECTION ( 'NONE',  ( 0.000000000000000000, 0.000000000000000000, -1.000000000000000000 ) ) ;
#12606=CARTESIAN_POINT ( 'NONE',  ( -240.4767932493553531, -3.790394256708240484, -11.38565896274289280 ) ) ;
#12607=CARTESIAN_POINT ( 'NONE',  ( -229.6889200636375108, -1.000000000000000000, 11.95826074310140008 ) ) ;
#12647=DIRECTION ( 'NONE',  ( 1.000000000000000000, 0.000000000000000000, 0.000000000000000000 ) ) ;
#12648=CARTESIAN_POINT ( 'NONE',  ( -239.2285245180114828, 1.532942925007542145, 11.90165677312966785 ) ) ;
#12675=CARTESIAN_POINT ( 'NONE',  ( -229.7802203235890204, -6.580825742931379452, 10.06232612585050035 ) ) ;
#12685=CARTESIAN_POINT ( 'NONE',  ( -249.7118339206215012, 9.997999799959989886, 6.636264009214830395 ) ) ;
#12708=CARTESIAN_POINT ( 'NONE',  ( -238.7400358149041324, 0.4567369020058948959, 11.99149615616909514 ) ) ;
#12710=CARTESIAN_POINT ( 'NONE',  ( -249.0734550459510785, -9.965425394270200243, 6.685150203391385659 ) ) ;
#12711=CIRCLE ( 'NONE', #4827, 240.2352941176469869 ) ;
#12713=CARTESIAN_POINT ( 'NONE',  ( -229.7895871136148003, 6.880706567532733686, 9.838484686103685206 ) ) ;
#12722=CARTESIAN_POINT ( 'NONE',  ( -241.1581829740684668, 5.108108803741933102, 10.85886904359302818 ) ) ;
#12723=EDGE_CURVE ( 'NONE', #5558, #4886, #12711, .T. ) ;
#12763=SHAPE_REPRESENTATION_RELATIONSHIP ( 'NONE' , 'NONE' ,  #4340, #3952 ) ;
#12774=CARTESIAN_POINT ( 'NONE',  ( -249.7800409167773807, -11.57739048714482522, 3.170426907214261458 ) ) ;
#12785=VERTEX_POINT ( 'NONE', #5931 ) ;
#12789=LINE ( 'NONE', #12531, #1284 ) ;
#12812=DIRECTION ( 'NONE',  ( -1.000000000000000000, 0.000000000000000000, 0.000000000000000000 ) ) ;
#12826=AXIS2_PLACEMENT_3D ( 'NONE', #7208, #2927, #7013 ) ;
#12840=CARTESIAN_POINT ( 'NONE',  ( 0.000000000000000000, 0.000000000000000000, 0.000000000000000000 ) ) ;
#12846=CARTESIAN_POINT ( 'NONE',  ( -241.3346421314001020, -5.383590977517163978, 10.72461093951733169 ) ) ;
#12849=CARTESIAN_POINT ( 'NONE',  ( -229.9857278087561951, 11.72347515457171419, 2.588372091913021755 ) ) ;
#12853=CIRCLE ( 'NONE', #10517, 230.0000000000000000 ) ;
#12869=CARTESIAN_POINT ( 'NONE',  ( -241.5877467159411083, -5.754636831476545922, -10.53299718410284314 ) ) ;
#12870=CARTESIAN_POINT ( 'NONE',  ( -229.7631934145547632, -5.935281959122680639, -10.43610481315899996 ) ) ;
#12885=FACE_OUTER_BOUND ( 'NONE', #6026, .T. ) ;
#12899=ADVANCED_FACE ( 'NONE', ( #5913 ), #6338, .F. ) ;
#12910=CARTESIAN_POINT ( 'NONE',  ( -244.6143483479685869, -8.518413533159836959, 8.452629830878873207 ) ) ;
#12914=CARTESIAN_POINT ( 'NONE',  ( -233.0000000000000000, -1.000000000000000000, -12.50000000000000000 ) ) ;
#12932=CARTESIAN_POINT ( 'NONE',  ( -246.7640704946416861, -9.498771479503499648, -7.332983348641192833 ) ) ;
#12934=CARTESIAN_POINT ( 'NONE',  ( -229.9651640739562879, -11.31348253173457152, -4.017925228533020032 ) ) ;
#12936=ORIENTED_EDGE ( 'NONE', *, *, #12587, .F. ) ;
#12978=CARTESIAN_POINT ( 'NONE',  ( -241.3126941818472631, -5.350247869156489422, 10.74127079069803514 ) ) ;
#12979=CARTESIAN_POINT ( 'NONE',  ( -239.6569666423348792, 1.960938215982088728, -11.83870082074197860 ) ) ;
#12985=VERTEX_POINT ( 'NONE', #8911 ) ;
#12993=FACE_OUTER_BOUND ( 'NONE', #1509, .T. ) ;
#12995=CARTESIAN_POINT ( 'NONE',  ( -240.5991998575718185, 4.074980142617108392, 11.29000474999590331 ) ) ;
#13001=APPLICATION_CONTEXT ( 'automotive_design' ) ;
#13018=CARTESIAN_POINT ( 'NONE',  ( -239.3393815604536883, -1.669038146043678950, 11.88372659485297689 ) ) ;
#13026=CARTESIAN_POINT ( 'NONE',  ( -238.7054577244453242, -0.2141779405393015034, -11.99854502521326793 ) ) ;
#13036=TOROIDAL_SURFACE ( 'NONE', #3667, 250.0000000000000000, 10.00000000000000000 ) ;
ENDSEC;
END-ISO-10303-21;
